ISO-10303-21;
HEADER;
/* Generated by software containing ST-Developer
 * from STEP Tools, Inc. (www.steptools.com) 
 */

FILE_DESCRIPTION(
/* description */ (''),
/* implementation_level */ '2;1');

FILE_NAME(
/* name */ '03_Journal_Bearing_D11.step',
/* time_stamp */ '2026-10-25T01:10:36-07:00',
/* author */ (''),
/* organization */ (''),
/* preprocessor_version */ 'ST-DEVELOPER v20.2',
/* originating_system */ 'Autodesk Translation Framework v15.15.0.0',
/* authorisation */ '');

FILE_SCHEMA (('AUTOMOTIVE_DESIGN { 1 0 10303 214 3 1 1 }'));
ENDSEC;

DATA;
#10=MECHANICAL_DESIGN_GEOMETRIC_PRESENTATION_REPRESENTATION('',(#1303),#60365);
#75=SHAPE_REPRESENTATION_RELATIONSHIP('SRR','None',#60415,#85);
#85=ADVANCED_BREP_SHAPE_REPRESENTATION('',(#95),#60363);
#95=MANIFOLD_SOLID_BREP('Body1',#18305);
#246=FACE_BOUND('',#3113,.T.);
#247=FACE_BOUND('',#3114,.T.);
#248=FACE_BOUND('',#3115,.T.);
#249=FACE_BOUND('',#3117,.T.);
#250=FACE_BOUND('',#3119,.T.);
#251=FACE_BOUND('',#3125,.T.);
#252=FACE_BOUND('',#3128,.T.);
#253=FACE_BOUND('',#3129,.T.);
#254=FACE_BOUND('',#3130,.T.);
#255=FACE_BOUND('',#3131,.T.);
#256=FACE_BOUND('',#3132,.T.);
#257=FACE_BOUND('',#3133,.T.);
#258=FACE_BOUND('',#3134,.T.);
#259=FACE_BOUND('',#3137,.T.);
#663=PLANE('',#19441);
#664=PLANE('',#19446);
#665=PLANE('',#19448);
#666=PLANE('',#19453);
#667=PLANE('',#19455);
#668=PLANE('',#19460);
#669=PLANE('',#19462);
#670=PLANE('',#19467);
#671=PLANE('',#19476);
#672=PLANE('',#19478);
#673=PLANE('',#19488);
#674=PLANE('',#19496);
#968=CONICAL_SURFACE('',#19482,8.6,0.785398163397449);
#969=CONICAL_SURFACE('',#19486,8.6,0.785398163397448);
#970=CONICAL_SURFACE('',#19490,5.67,0.78539816339745);
#971=CONICAL_SURFACE('',#19494,5.67,0.785398163397451);
#1303=STYLED_ITEM('',(#60527),#95);
#2083=FACE_OUTER_BOUND('',#3096,.T.);
#2084=FACE_OUTER_BOUND('',#3097,.T.);
#2085=FACE_OUTER_BOUND('',#3098,.T.);
#2086=FACE_OUTER_BOUND('',#3099,.T.);
#2087=FACE_OUTER_BOUND('',#3100,.T.);
#2088=FACE_OUTER_BOUND('',#3101,.T.);
#2089=FACE_OUTER_BOUND('',#3102,.T.);
#2090=FACE_OUTER_BOUND('',#3103,.T.);
#2091=FACE_OUTER_BOUND('',#3104,.T.);
#2092=FACE_OUTER_BOUND('',#3105,.T.);
#2093=FACE_OUTER_BOUND('',#3106,.T.);
#2094=FACE_OUTER_BOUND('',#3107,.T.);
#2095=FACE_OUTER_BOUND('',#3108,.T.);
#2096=FACE_OUTER_BOUND('',#3109,.T.);
#2097=FACE_OUTER_BOUND('',#3110,.T.);
#2098=FACE_OUTER_BOUND('',#3111,.T.);
#2099=FACE_OUTER_BOUND('',#3112,.T.);
#2100=FACE_OUTER_BOUND('',#3116,.T.);
#2101=FACE_OUTER_BOUND('',#3118,.T.);
#2102=FACE_OUTER_BOUND('',#3120,.T.);
#2103=FACE_OUTER_BOUND('',#3121,.T.);
#2104=FACE_OUTER_BOUND('',#3122,.T.);
#2105=FACE_OUTER_BOUND('',#3123,.T.);
#2106=FACE_OUTER_BOUND('',#3124,.T.);
#2107=FACE_OUTER_BOUND('',#3126,.T.);
#2108=FACE_OUTER_BOUND('',#3127,.T.);
#2109=FACE_OUTER_BOUND('',#3135,.T.);
#2110=FACE_OUTER_BOUND('',#3136,.T.);
#3096=EDGE_LOOP('',(#16153,#16154));
#3097=EDGE_LOOP('',(#16155,#16156,#16157,#16158));
#3098=EDGE_LOOP('',(#16159,#16160));
#3099=EDGE_LOOP('',(#16161,#16162));
#3100=EDGE_LOOP('',(#16163,#16164,#16165,#16166));
#3101=EDGE_LOOP('',(#16167,#16168));
#3102=EDGE_LOOP('',(#16169,#16170));
#3103=EDGE_LOOP('',(#16171,#16172,#16173,#16174));
#3104=EDGE_LOOP('',(#16175,#16176));
#3105=EDGE_LOOP('',(#16177,#16178));
#3106=EDGE_LOOP('',(#16179,#16180,#16181,#16182));
#3107=EDGE_LOOP('',(#16183,#16184));
#3108=EDGE_LOOP('',(#16185,#16186,#16187,#16188,#16189,#16190));
#3109=EDGE_LOOP('',(#16191,#16192,#16193,#16194,#16195,#16196));
#3110=EDGE_LOOP('',(#16197,#16198,#16199,#16200,#16201,#16202,#16203));
#3111=EDGE_LOOP('',(#16204,#16205,#16206,#16207,#16208,#16209));
#3112=EDGE_LOOP('',(#16210,#16211,#16212,#16213,#16214,#16215,#16216,#16217));
#3113=EDGE_LOOP('',(#16218,#16219));
#3114=EDGE_LOOP('',(#16220,#16221));
#3115=EDGE_LOOP('',(#16222,#16223));
#3116=EDGE_LOOP('',(#16224));
#3117=EDGE_LOOP('',(#16225));
#3118=EDGE_LOOP('',(#16226));
#3119=EDGE_LOOP('',(#16227));
#3120=EDGE_LOOP('',(#16228,#16229,#16230,#16231));
#3121=EDGE_LOOP('',(#16232,#16233,#16234,#16235));
#3122=EDGE_LOOP('',(#16236,#16237,#16238,#16239));
#3123=EDGE_LOOP('',(#16240,#16241,#16242,#16243));
#3124=EDGE_LOOP('',(#16244));
#3125=EDGE_LOOP('',(#16245));
#3126=EDGE_LOOP('',(#16246,#16247,#16248,#16249));
#3127=EDGE_LOOP('',(#16250,#16251,#16252,#16253,#16254,#16255,#16256,#16257,
#16258));
#3128=EDGE_LOOP('',(#16259,#16260,#16261,#16262));
#3129=EDGE_LOOP('',(#16263,#16264,#16265,#16266));
#3130=EDGE_LOOP('',(#16267,#16268,#16269,#16270));
#3131=EDGE_LOOP('',(#16271,#16272,#16273,#16274));
#3132=EDGE_LOOP('',(#16275,#16276));
#3133=EDGE_LOOP('',(#16277,#16278));
#3134=EDGE_LOOP('',(#16279,#16280));
#3135=EDGE_LOOP('',(#16281,#16282,#16283,#16284));
#3136=EDGE_LOOP('',(#16285));
#3137=EDGE_LOOP('',(#16286));
#3669=CIRCLE('',#19442,5.52);
#3670=CIRCLE('',#19443,0.6);
#3671=CIRCLE('',#19445,0.6);
#3672=CIRCLE('',#19447,5.52);
#3673=CIRCLE('',#19449,5.52);
#3674=CIRCLE('',#19450,0.6);
#3675=CIRCLE('',#19452,0.6);
#3676=CIRCLE('',#19454,5.52);
#3677=CIRCLE('',#19456,5.52);
#3678=CIRCLE('',#19457,0.6);
#3679=CIRCLE('',#19459,0.6);
#3680=CIRCLE('',#19461,5.52);
#3681=CIRCLE('',#19463,5.52);
#3682=CIRCLE('',#19464,0.6);
#3683=CIRCLE('',#19466,0.6);
#3684=CIRCLE('',#19468,5.52);
#3685=CIRCLE('',#19474,8.45);
#3686=CIRCLE('',#19475,8.45);
#3687=CIRCLE('',#19477,8.8);
#3688=CIRCLE('',#19479,8.8);
#3689=CIRCLE('',#19481,8.8);
#3690=CIRCLE('',#19483,8.8);
#3691=CIRCLE('',#19484,8.4);
#3692=CIRCLE('',#19487,8.4);
#3693=CIRCLE('',#19489,5.82);
#3694=CIRCLE('',#19491,5.52);
#3695=CIRCLE('',#19493,5.52);
#3696=CIRCLE('',#19495,5.82);
#4483=B_SPLINE_CURVE_WITH_KNOTS('',3,(#59035,#59036,#59037,#59038,#59039,
#59040,#59041,#59042,#59043,#59044,#59045,#59046,#59047,#59048,#59049,#59050,
#59051,#59052),.UNSPECIFIED.,.F.,.F.,(4,2,2,2,2,2,2,2,4),(0.165944509231404,
0.207430432450317,0.24891635566923,0.290402687066019,0.331889018462808,
0.373375349859597,0.414861681256386,0.456347604475299,0.497833527694212),
 .UNSPECIFIED.);
#4484=B_SPLINE_CURVE_WITH_KNOTS('',3,(#59053,#59054,#59055,#59056,#59057,
#59058,#59059,#59060,#59061,#59062,#59063,#59064,#59065,#59066,#59067,#59068,
#59069,#59070,#59071),.UNSPECIFIED.,.F.,.F.,(4,2,2,2,3,2,2,2,4),(0.497833527694212,
0.539319450913125,0.580805374132038,0.622291705528827,0.663778036925616,
0.705264368322405,0.746750699719194,0.788236622938107,0.82972254615702),
 .UNSPECIFIED.);
#4485=B_SPLINE_CURVE_WITH_KNOTS('',3,(#59075,#59076,#59077,#59078,#59079,
#59080,#59081,#59082,#59083,#59084),.UNSPECIFIED.,.F.,.F.,(4,2,2,2,4),(0.,
0.0415565701679523,0.0831131403359046,0.12466741609854,0.166221691861175),
 .UNSPECIFIED.);
#4486=B_SPLINE_CURVE_WITH_KNOTS('',3,(#59085,#59086,#59087,#59088,#59089,
#59090,#59091,#59092,#59093,#59094,#59095,#59096,#59097,#59098,#59099,#59100,
#59101,#59102,#59103,#59104,#59105,#59106,#59107,#59108,#59109,#59110),
 .UNSPECIFIED.,.F.,.F.,(4,2,2,2,2,2,2,2,2,2,2,2,4),(0.166221691861175,0.20777596762381,
0.249330243386446,0.290886813554398,0.33244338372235,0.373999953890303,
0.415556524058255,0.45711079982089,0.498665075583526,0.540219351346161,
0.581773627108796,0.623330197276748,0.664886767444701),.UNSPECIFIED.);
#4487=B_SPLINE_CURVE_WITH_KNOTS('',3,(#59114,#59115,#59116,#59117,#59118,
#59119,#59120,#59121,#59122,#59123,#59124,#59125,#59126,#59127,#59128,#59129,
#59130,#59131),.UNSPECIFIED.,.F.,.F.,(4,2,2,2,2,2,2,2,4),(0.165944509231404,
0.207430432450317,0.24891635566923,0.290402687066019,0.331889018462808,
0.373375349859597,0.414861681256386,0.456347604475299,0.497833527694212),
 .UNSPECIFIED.);
#4488=B_SPLINE_CURVE_WITH_KNOTS('',3,(#59132,#59133,#59134,#59135,#59136,
#59137,#59138,#59139,#59140,#59141,#59142,#59143,#59144,#59145,#59146,#59147,
#59148,#59149,#59150),.UNSPECIFIED.,.F.,.F.,(4,2,2,2,3,2,2,2,4),(0.497833527694212,
0.539319450913125,0.580805374132038,0.622291705528827,0.663778036925616,
0.705264368322405,0.746750699719194,0.788236622938107,0.82972254615702),
 .UNSPECIFIED.);
#4489=B_SPLINE_CURVE_WITH_KNOTS('',3,(#59154,#59155,#59156,#59157,#59158,
#59159,#59160,#59161,#59162,#59163),.UNSPECIFIED.,.F.,.F.,(4,2,2,2,4),(0.,
0.0415565701679523,0.0831131403359046,0.12466741609854,0.166221691861175),
 .UNSPECIFIED.);
#4490=B_SPLINE_CURVE_WITH_KNOTS('',3,(#59164,#59165,#59166,#59167,#59168,
#59169,#59170,#59171,#59172,#59173,#59174,#59175,#59176,#59177,#59178,#59179,
#59180,#59181,#59182,#59183,#59184,#59185,#59186,#59187,#59188,#59189),
 .UNSPECIFIED.,.F.,.F.,(4,2,2,2,2,2,2,2,2,2,2,2,4),(0.166221691861175,0.20777596762381,
0.249330243386446,0.290886813554398,0.33244338372235,0.373999953890303,
0.415556524058255,0.45711079982089,0.498665075583525,0.540219351346161,
0.581773627108796,0.623330197276748,0.664886767444701),.UNSPECIFIED.);
#4491=B_SPLINE_CURVE_WITH_KNOTS('',3,(#59193,#59194,#59195,#59196,#59197,
#59198,#59199,#59200,#59201,#59202,#59203,#59204,#59205,#59206,#59207,#59208,
#59209,#59210),.UNSPECIFIED.,.F.,.F.,(4,2,2,2,2,2,2,2,4),(0.165944509231404,
0.207430432450317,0.24891635566923,0.290402687066019,0.331889018462808,
0.373375349859597,0.414861681256386,0.456347604475299,0.497833527694212),
 .UNSPECIFIED.);
#4492=B_SPLINE_CURVE_WITH_KNOTS('',3,(#59211,#59212,#59213,#59214,#59215,
#59216,#59217,#59218,#59219,#59220,#59221,#59222,#59223,#59224,#59225,#59226,
#59227,#59228,#59229),.UNSPECIFIED.,.F.,.F.,(4,2,2,2,3,2,2,2,4),(0.497833527694212,
0.539319450913125,0.580805374132038,0.622291705528827,0.663778036925616,
0.705264368322405,0.746750699719194,0.788236622938107,0.82972254615702),
 .UNSPECIFIED.);
#4493=B_SPLINE_CURVE_WITH_KNOTS('',3,(#59233,#59234,#59235,#59236,#59237,
#59238,#59239,#59240,#59241,#59242),.UNSPECIFIED.,.F.,.F.,(4,2,2,2,4),(0.,
0.0415565701679523,0.0831131403359045,0.12466741609854,0.166221691861175),
 .UNSPECIFIED.);
#4494=B_SPLINE_CURVE_WITH_KNOTS('',3,(#59244,#59245,#59246,#59247,#59248,
#59249,#59250,#59251,#59252,#59253),.UNSPECIFIED.,.F.,.F.,(4,2,2,2,4),(0.498665075583525,
0.540219351346161,0.581773627108796,0.623330197276748,0.664886767444701),
 .UNSPECIFIED.);
#4495=B_SPLINE_CURVE_WITH_KNOTS('',3,(#59254,#59255,#59256,#59257,#59258,
#59259,#59260,#59261,#59262,#59263,#59264,#59265,#59266,#59267,#59268,#59269,
#59270,#59271),.UNSPECIFIED.,.F.,.F.,(4,2,2,2,2,2,2,2,4),(0.166221691861175,
0.20777596762381,0.249330243386446,0.290886813554398,0.33244338372235,0.373999953890303,
0.415556524058255,0.45711079982089,0.498665075583525),.UNSPECIFIED.);
#4496=B_SPLINE_CURVE_WITH_KNOTS('',3,(#59275,#59276,#59277,#59278,#59279,
#59280,#59281,#59282,#59283,#59284,#59285,#59286,#59287,#59288,#59289,#59290,
#59291,#59292),.UNSPECIFIED.,.F.,.F.,(4,2,2,2,2,2,2,2,4),(0.165944509231404,
0.207430432450317,0.24891635566923,0.290402687066019,0.331889018462808,
0.373375349859597,0.414861681256386,0.456347604475299,0.497833527694212),
 .UNSPECIFIED.);
#4497=B_SPLINE_CURVE_WITH_KNOTS('',3,(#59293,#59294,#59295,#59296,#59297,
#59298,#59299,#59300,#59301,#59302,#59303,#59304,#59305,#59306,#59307,#59308,
#59309,#59310,#59311),.UNSPECIFIED.,.F.,.F.,(4,2,2,2,3,2,2,2,4),(0.497833527694212,
0.539319450913125,0.580805374132038,0.622291705528827,0.663778036925616,
0.705264368322405,0.746750699719194,0.788236622938107,0.82972254615702),
 .UNSPECIFIED.);
#4498=B_SPLINE_CURVE_WITH_KNOTS('',3,(#59315,#59316,#59317,#59318,#59319,
#59320,#59321,#59322,#59323,#59324),.UNSPECIFIED.,.F.,.F.,(4,2,2,2,4),(0.,
0.0415565701679523,0.0831131403359046,0.12466741609854,0.166221691861175),
 .UNSPECIFIED.);
#4499=B_SPLINE_CURVE_WITH_KNOTS('',3,(#59325,#59326,#59327,#59328,#59329,
#59330,#59331,#59332,#59333,#59334,#59335,#59336,#59337,#59338,#59339,#59340,
#59341,#59342,#59343,#59344,#59345,#59346,#59347,#59348,#59349,#59350),
 .UNSPECIFIED.,.F.,.F.,(4,2,2,2,2,2,2,2,2,2,2,2,4),(0.166221691861175,0.20777596762381,
0.249330243386446,0.290886813554398,0.33244338372235,0.373999953890303,
0.415556524058255,0.45711079982089,0.498665075583525,0.540219351346161,
0.581773627108796,0.623330197276748,0.664886767444701),.UNSPECIFIED.);
#5434=LINE('',#58987,#6846);
#5435=LINE('',#58990,#6847);
#5436=LINE('',#59000,#6848);
#5437=LINE('',#59003,#6849);
#5438=LINE('',#59013,#6850);
#5439=LINE('',#59016,#6851);
#5440=LINE('',#59026,#6852);
#5441=LINE('',#59029,#6853);
#5442=LINE('',#59073,#6854);
#5443=LINE('',#59152,#6855);
#5444=LINE('',#59231,#6856);
#5445=LINE('',#59313,#6857);
#5446=LINE('',#59354,#6858);
#5447=LINE('',#59356,#6859);
#5448=LINE('',#59367,#6860);
#5449=LINE('',#59372,#6861);
#5450=LINE('',#59375,#6862);
#5451=LINE('',#59379,#6863);
#5452=LINE('',#59385,#6864);
#5453=LINE('',#59388,#6865);
#5454=LINE('',#59390,#6866);
#5455=LINE('',#59394,#6867);
#6846=VECTOR('',#22666,10.);
#6847=VECTOR('',#22669,10.);
#6848=VECTOR('',#22682,10.);
#6849=VECTOR('',#22685,10.);
#6850=VECTOR('',#22698,10.);
#6851=VECTOR('',#22701,10.);
#6852=VECTOR('',#22714,10.);
#6853=VECTOR('',#22717,10.);
#6854=VECTOR('',#22724,1.1);
#6855=VECTOR('',#22727,1.1);
#6856=VECTOR('',#22730,1.1);
#6857=VECTOR('',#22733,1.1);
#6858=VECTOR('',#22738,8.45);
#6859=VECTOR('',#22739,8.45);
#6860=VECTOR('',#22754,8.8);
#6861=VECTOR('',#22759,8.6);
#6862=VECTOR('',#22764,8.8);
#6863=VECTOR('',#22769,8.6);
#6864=VECTOR('',#22776,5.67);
#6865=VECTOR('',#22781,5.52);
#6866=VECTOR('',#22782,5.52);
#6867=VECTOR('',#22787,5.67);
#8762=VERTEX_POINT('',#58981);
#8763=VERTEX_POINT('',#58982);
#8764=VERTEX_POINT('',#58986);
#8765=VERTEX_POINT('',#58988);
#8766=VERTEX_POINT('',#58994);
#8767=VERTEX_POINT('',#58995);
#8768=VERTEX_POINT('',#58999);
#8769=VERTEX_POINT('',#59001);
#8770=VERTEX_POINT('',#59007);
#8771=VERTEX_POINT('',#59008);
#8772=VERTEX_POINT('',#59012);
#8773=VERTEX_POINT('',#59014);
#8774=VERTEX_POINT('',#59020);
#8775=VERTEX_POINT('',#59021);
#8776=VERTEX_POINT('',#59025);
#8777=VERTEX_POINT('',#59027);
#8778=VERTEX_POINT('',#59033);
#8779=VERTEX_POINT('',#59034);
#8780=VERTEX_POINT('',#59072);
#8781=VERTEX_POINT('',#59074);
#8782=VERTEX_POINT('',#59112);
#8783=VERTEX_POINT('',#59113);
#8784=VERTEX_POINT('',#59151);
#8785=VERTEX_POINT('',#59153);
#8786=VERTEX_POINT('',#59191);
#8787=VERTEX_POINT('',#59192);
#8788=VERTEX_POINT('',#59230);
#8789=VERTEX_POINT('',#59232);
#8790=VERTEX_POINT('',#59243);
#8791=VERTEX_POINT('',#59273);
#8792=VERTEX_POINT('',#59274);
#8793=VERTEX_POINT('',#59312);
#8794=VERTEX_POINT('',#59314);
#8795=VERTEX_POINT('',#59352);
#8796=VERTEX_POINT('',#59355);
#8797=VERTEX_POINT('',#59359);
#8798=VERTEX_POINT('',#59362);
#8799=VERTEX_POINT('',#59365);
#8800=VERTEX_POINT('',#59369);
#8801=VERTEX_POINT('',#59371);
#8802=VERTEX_POINT('',#59377);
#8803=VERTEX_POINT('',#59381);
#8804=VERTEX_POINT('',#59384);
#8805=VERTEX_POINT('',#59389);
#8806=VERTEX_POINT('',#59393);
#11284=EDGE_CURVE('',#8762,#8763,#3669,.T.);
#11285=EDGE_CURVE('',#8762,#8763,#3670,.T.);
#11286=EDGE_CURVE('',#8764,#8762,#5434,.T.);
#11287=EDGE_CURVE('',#8764,#8765,#3671,.T.);
#11288=EDGE_CURVE('',#8763,#8765,#5435,.T.);
#11289=EDGE_CURVE('',#8765,#8764,#3672,.T.);
#11290=EDGE_CURVE('',#8766,#8767,#3673,.T.);
#11291=EDGE_CURVE('',#8766,#8767,#3674,.T.);
#11292=EDGE_CURVE('',#8768,#8766,#5436,.T.);
#11293=EDGE_CURVE('',#8768,#8769,#3675,.T.);
#11294=EDGE_CURVE('',#8767,#8769,#5437,.T.);
#11295=EDGE_CURVE('',#8769,#8768,#3676,.T.);
#11296=EDGE_CURVE('',#8770,#8771,#3677,.T.);
#11297=EDGE_CURVE('',#8770,#8771,#3678,.T.);
#11298=EDGE_CURVE('',#8772,#8770,#5438,.T.);
#11299=EDGE_CURVE('',#8772,#8773,#3679,.T.);
#11300=EDGE_CURVE('',#8771,#8773,#5439,.T.);
#11301=EDGE_CURVE('',#8773,#8772,#3680,.T.);
#11302=EDGE_CURVE('',#8774,#8775,#3681,.T.);
#11303=EDGE_CURVE('',#8774,#8775,#3682,.T.);
#11304=EDGE_CURVE('',#8776,#8774,#5440,.T.);
#11305=EDGE_CURVE('',#8776,#8777,#3683,.T.);
#11306=EDGE_CURVE('',#8775,#8777,#5441,.T.);
#11307=EDGE_CURVE('',#8777,#8776,#3684,.T.);
#11308=EDGE_CURVE('',#8778,#8779,#4483,.T.);
#11309=EDGE_CURVE('',#8779,#8778,#4484,.T.);
#11310=EDGE_CURVE('',#8779,#8780,#5442,.T.);
#11311=EDGE_CURVE('',#8781,#8780,#4485,.T.);
#11312=EDGE_CURVE('',#8780,#8781,#4486,.T.);
#11313=EDGE_CURVE('',#8782,#8783,#4487,.T.);
#11314=EDGE_CURVE('',#8783,#8782,#4488,.T.);
#11315=EDGE_CURVE('',#8783,#8784,#5443,.T.);
#11316=EDGE_CURVE('',#8785,#8784,#4489,.T.);
#11317=EDGE_CURVE('',#8784,#8785,#4490,.T.);
#11318=EDGE_CURVE('',#8786,#8787,#4491,.T.);
#11319=EDGE_CURVE('',#8787,#8786,#4492,.T.);
#11320=EDGE_CURVE('',#8787,#8788,#5444,.T.);
#11321=EDGE_CURVE('',#8789,#8788,#4493,.T.);
#11322=EDGE_CURVE('',#8790,#8789,#4494,.T.);
#11323=EDGE_CURVE('',#8788,#8790,#4495,.T.);
#11324=EDGE_CURVE('',#8791,#8792,#4496,.T.);
#11325=EDGE_CURVE('',#8792,#8791,#4497,.T.);
#11326=EDGE_CURVE('',#8792,#8793,#5445,.T.);
#11327=EDGE_CURVE('',#8794,#8793,#4498,.T.);
#11328=EDGE_CURVE('',#8793,#8794,#4499,.T.);
#11329=EDGE_CURVE('',#8795,#8795,#3685,.T.);
#11330=EDGE_CURVE('',#8795,#8787,#5446,.T.);
#11331=EDGE_CURVE('',#8786,#8796,#5447,.T.);
#11332=EDGE_CURVE('',#8796,#8796,#3686,.T.);
#11333=EDGE_CURVE('',#8797,#8797,#3687,.T.);
#11334=EDGE_CURVE('',#8798,#8798,#3688,.T.);
#11335=EDGE_CURVE('',#8799,#8799,#3689,.T.);
#11336=EDGE_CURVE('',#8799,#8798,#5448,.T.);
#11337=EDGE_CURVE('',#8800,#8800,#3690,.T.);
#11338=EDGE_CURVE('',#8800,#8801,#5449,.T.);
#11339=EDGE_CURVE('',#8801,#8801,#3691,.T.);
#11340=EDGE_CURVE('',#8797,#8800,#5450,.T.);
#11341=EDGE_CURVE('',#8802,#8802,#3692,.T.);
#11342=EDGE_CURVE('',#8802,#8799,#5451,.T.);
#11343=EDGE_CURVE('',#8803,#8803,#3693,.T.);
#11344=EDGE_CURVE('',#8803,#8804,#5452,.T.);
#11345=EDGE_CURVE('',#8804,#8804,#3694,.T.);
#11346=EDGE_CURVE('',#8804,#8790,#5453,.T.);
#11347=EDGE_CURVE('',#8788,#8805,#5454,.T.);
#11348=EDGE_CURVE('',#8805,#8805,#3695,.T.);
#11349=EDGE_CURVE('',#8805,#8806,#5455,.T.);
#11350=EDGE_CURVE('',#8806,#8806,#3696,.T.);
#16153=ORIENTED_EDGE('',*,*,#11284,.F.);
#16154=ORIENTED_EDGE('',*,*,#11285,.T.);
#16155=ORIENTED_EDGE('',*,*,#11286,.F.);
#16156=ORIENTED_EDGE('',*,*,#11287,.T.);
#16157=ORIENTED_EDGE('',*,*,#11288,.F.);
#16158=ORIENTED_EDGE('',*,*,#11285,.F.);
#16159=ORIENTED_EDGE('',*,*,#11289,.F.);
#16160=ORIENTED_EDGE('',*,*,#11287,.F.);
#16161=ORIENTED_EDGE('',*,*,#11290,.F.);
#16162=ORIENTED_EDGE('',*,*,#11291,.T.);
#16163=ORIENTED_EDGE('',*,*,#11292,.F.);
#16164=ORIENTED_EDGE('',*,*,#11293,.T.);
#16165=ORIENTED_EDGE('',*,*,#11294,.F.);
#16166=ORIENTED_EDGE('',*,*,#11291,.F.);
#16167=ORIENTED_EDGE('',*,*,#11295,.F.);
#16168=ORIENTED_EDGE('',*,*,#11293,.F.);
#16169=ORIENTED_EDGE('',*,*,#11296,.F.);
#16170=ORIENTED_EDGE('',*,*,#11297,.T.);
#16171=ORIENTED_EDGE('',*,*,#11298,.F.);
#16172=ORIENTED_EDGE('',*,*,#11299,.T.);
#16173=ORIENTED_EDGE('',*,*,#11300,.F.);
#16174=ORIENTED_EDGE('',*,*,#11297,.F.);
#16175=ORIENTED_EDGE('',*,*,#11301,.F.);
#16176=ORIENTED_EDGE('',*,*,#11299,.F.);
#16177=ORIENTED_EDGE('',*,*,#11302,.F.);
#16178=ORIENTED_EDGE('',*,*,#11303,.T.);
#16179=ORIENTED_EDGE('',*,*,#11304,.F.);
#16180=ORIENTED_EDGE('',*,*,#11305,.T.);
#16181=ORIENTED_EDGE('',*,*,#11306,.F.);
#16182=ORIENTED_EDGE('',*,*,#11303,.F.);
#16183=ORIENTED_EDGE('',*,*,#11307,.F.);
#16184=ORIENTED_EDGE('',*,*,#11305,.F.);
#16185=ORIENTED_EDGE('',*,*,#11308,.F.);
#16186=ORIENTED_EDGE('',*,*,#11309,.F.);
#16187=ORIENTED_EDGE('',*,*,#11310,.T.);
#16188=ORIENTED_EDGE('',*,*,#11311,.F.);
#16189=ORIENTED_EDGE('',*,*,#11312,.F.);
#16190=ORIENTED_EDGE('',*,*,#11310,.F.);
#16191=ORIENTED_EDGE('',*,*,#11313,.F.);
#16192=ORIENTED_EDGE('',*,*,#11314,.F.);
#16193=ORIENTED_EDGE('',*,*,#11315,.T.);
#16194=ORIENTED_EDGE('',*,*,#11316,.F.);
#16195=ORIENTED_EDGE('',*,*,#11317,.F.);
#16196=ORIENTED_EDGE('',*,*,#11315,.F.);
#16197=ORIENTED_EDGE('',*,*,#11318,.F.);
#16198=ORIENTED_EDGE('',*,*,#11319,.F.);
#16199=ORIENTED_EDGE('',*,*,#11320,.T.);
#16200=ORIENTED_EDGE('',*,*,#11321,.F.);
#16201=ORIENTED_EDGE('',*,*,#11322,.F.);
#16202=ORIENTED_EDGE('',*,*,#11323,.F.);
#16203=ORIENTED_EDGE('',*,*,#11320,.F.);
#16204=ORIENTED_EDGE('',*,*,#11324,.F.);
#16205=ORIENTED_EDGE('',*,*,#11325,.F.);
#16206=ORIENTED_EDGE('',*,*,#11326,.T.);
#16207=ORIENTED_EDGE('',*,*,#11327,.F.);
#16208=ORIENTED_EDGE('',*,*,#11328,.F.);
#16209=ORIENTED_EDGE('',*,*,#11326,.F.);
#16210=ORIENTED_EDGE('',*,*,#11329,.T.);
#16211=ORIENTED_EDGE('',*,*,#11330,.T.);
#16212=ORIENTED_EDGE('',*,*,#11319,.T.);
#16213=ORIENTED_EDGE('',*,*,#11331,.T.);
#16214=ORIENTED_EDGE('',*,*,#11332,.F.);
#16215=ORIENTED_EDGE('',*,*,#11331,.F.);
#16216=ORIENTED_EDGE('',*,*,#11318,.T.);
#16217=ORIENTED_EDGE('',*,*,#11330,.F.);
#16218=ORIENTED_EDGE('',*,*,#11308,.T.);
#16219=ORIENTED_EDGE('',*,*,#11309,.T.);
#16220=ORIENTED_EDGE('',*,*,#11313,.T.);
#16221=ORIENTED_EDGE('',*,*,#11314,.T.);
#16222=ORIENTED_EDGE('',*,*,#11324,.T.);
#16223=ORIENTED_EDGE('',*,*,#11325,.T.);
#16224=ORIENTED_EDGE('',*,*,#11333,.F.);
#16225=ORIENTED_EDGE('',*,*,#11329,.F.);
#16226=ORIENTED_EDGE('',*,*,#11334,.F.);
#16227=ORIENTED_EDGE('',*,*,#11332,.T.);
#16228=ORIENTED_EDGE('',*,*,#11335,.F.);
#16229=ORIENTED_EDGE('',*,*,#11336,.T.);
#16230=ORIENTED_EDGE('',*,*,#11334,.T.);
#16231=ORIENTED_EDGE('',*,*,#11336,.F.);
#16232=ORIENTED_EDGE('',*,*,#11337,.F.);
#16233=ORIENTED_EDGE('',*,*,#11338,.T.);
#16234=ORIENTED_EDGE('',*,*,#11339,.T.);
#16235=ORIENTED_EDGE('',*,*,#11338,.F.);
#16236=ORIENTED_EDGE('',*,*,#11333,.T.);
#16237=ORIENTED_EDGE('',*,*,#11340,.T.);
#16238=ORIENTED_EDGE('',*,*,#11337,.T.);
#16239=ORIENTED_EDGE('',*,*,#11340,.F.);
#16240=ORIENTED_EDGE('',*,*,#11341,.F.);
#16241=ORIENTED_EDGE('',*,*,#11342,.T.);
#16242=ORIENTED_EDGE('',*,*,#11335,.T.);
#16243=ORIENTED_EDGE('',*,*,#11342,.F.);
#16244=ORIENTED_EDGE('',*,*,#11341,.T.);
#16245=ORIENTED_EDGE('',*,*,#11343,.F.);
#16246=ORIENTED_EDGE('',*,*,#11343,.T.);
#16247=ORIENTED_EDGE('',*,*,#11344,.T.);
#16248=ORIENTED_EDGE('',*,*,#11345,.F.);
#16249=ORIENTED_EDGE('',*,*,#11344,.F.);
#16250=ORIENTED_EDGE('',*,*,#11345,.T.);
#16251=ORIENTED_EDGE('',*,*,#11346,.T.);
#16252=ORIENTED_EDGE('',*,*,#11322,.T.);
#16253=ORIENTED_EDGE('',*,*,#11321,.T.);
#16254=ORIENTED_EDGE('',*,*,#11347,.T.);
#16255=ORIENTED_EDGE('',*,*,#11348,.F.);
#16256=ORIENTED_EDGE('',*,*,#11347,.F.);
#16257=ORIENTED_EDGE('',*,*,#11323,.T.);
#16258=ORIENTED_EDGE('',*,*,#11346,.F.);
#16259=ORIENTED_EDGE('',*,*,#11288,.T.);
#16260=ORIENTED_EDGE('',*,*,#11289,.T.);
#16261=ORIENTED_EDGE('',*,*,#11286,.T.);
#16262=ORIENTED_EDGE('',*,*,#11284,.T.);
#16263=ORIENTED_EDGE('',*,*,#11294,.T.);
#16264=ORIENTED_EDGE('',*,*,#11295,.T.);
#16265=ORIENTED_EDGE('',*,*,#11292,.T.);
#16266=ORIENTED_EDGE('',*,*,#11290,.T.);
#16267=ORIENTED_EDGE('',*,*,#11300,.T.);
#16268=ORIENTED_EDGE('',*,*,#11301,.T.);
#16269=ORIENTED_EDGE('',*,*,#11298,.T.);
#16270=ORIENTED_EDGE('',*,*,#11296,.T.);
#16271=ORIENTED_EDGE('',*,*,#11306,.T.);
#16272=ORIENTED_EDGE('',*,*,#11307,.T.);
#16273=ORIENTED_EDGE('',*,*,#11304,.T.);
#16274=ORIENTED_EDGE('',*,*,#11302,.T.);
#16275=ORIENTED_EDGE('',*,*,#11311,.T.);
#16276=ORIENTED_EDGE('',*,*,#11312,.T.);
#16277=ORIENTED_EDGE('',*,*,#11316,.T.);
#16278=ORIENTED_EDGE('',*,*,#11317,.T.);
#16279=ORIENTED_EDGE('',*,*,#11327,.T.);
#16280=ORIENTED_EDGE('',*,*,#11328,.T.);
#16281=ORIENTED_EDGE('',*,*,#11348,.T.);
#16282=ORIENTED_EDGE('',*,*,#11349,.T.);
#16283=ORIENTED_EDGE('',*,*,#11350,.F.);
#16284=ORIENTED_EDGE('',*,*,#11349,.F.);
#16285=ORIENTED_EDGE('',*,*,#11339,.F.);
#16286=ORIENTED_EDGE('',*,*,#11350,.T.);
#17319=CYLINDRICAL_SURFACE('',#19444,0.6);
#17320=CYLINDRICAL_SURFACE('',#19451,0.6);
#17321=CYLINDRICAL_SURFACE('',#19458,0.6);
#17322=CYLINDRICAL_SURFACE('',#19465,0.6);
#17323=CYLINDRICAL_SURFACE('',#19469,1.1);
#17324=CYLINDRICAL_SURFACE('',#19470,1.1);
#17325=CYLINDRICAL_SURFACE('',#19471,1.1);
#17326=CYLINDRICAL_SURFACE('',#19472,1.1);
#17327=CYLINDRICAL_SURFACE('',#19473,8.45);
#17328=CYLINDRICAL_SURFACE('',#19480,8.8);
#17329=CYLINDRICAL_SURFACE('',#19485,8.8);
#17330=CYLINDRICAL_SURFACE('',#19492,5.52);
#18111=ADVANCED_FACE('',(#2083),#663,.T.);
#18112=ADVANCED_FACE('',(#2084),#17319,.F.);
#18113=ADVANCED_FACE('',(#2085),#664,.F.);
#18114=ADVANCED_FACE('',(#2086),#665,.T.);
#18115=ADVANCED_FACE('',(#2087),#17320,.F.);
#18116=ADVANCED_FACE('',(#2088),#666,.F.);
#18117=ADVANCED_FACE('',(#2089),#667,.T.);
#18118=ADVANCED_FACE('',(#2090),#17321,.F.);
#18119=ADVANCED_FACE('',(#2091),#668,.F.);
#18120=ADVANCED_FACE('',(#2092),#669,.T.);
#18121=ADVANCED_FACE('',(#2093),#17322,.F.);
#18122=ADVANCED_FACE('',(#2094),#670,.F.);
#18123=ADVANCED_FACE('',(#2095),#17323,.F.);
#18124=ADVANCED_FACE('',(#2096),#17324,.F.);
#18125=ADVANCED_FACE('',(#2097),#17325,.F.);
#18126=ADVANCED_FACE('',(#2098),#17326,.F.);
#18127=ADVANCED_FACE('',(#2099,#246,#247,#248),#17327,.T.);
#18128=ADVANCED_FACE('',(#2100,#249),#671,.F.);
#18129=ADVANCED_FACE('',(#2101,#250),#672,.F.);
#18130=ADVANCED_FACE('',(#2102),#17328,.T.);
#18131=ADVANCED_FACE('',(#2103),#968,.T.);
#18132=ADVANCED_FACE('',(#2104),#17329,.T.);
#18133=ADVANCED_FACE('',(#2105),#969,.T.);
#18134=ADVANCED_FACE('',(#2106,#251),#673,.T.);
#18135=ADVANCED_FACE('',(#2107),#970,.F.);
#18136=ADVANCED_FACE('',(#2108,#252,#253,#254,#255,#256,#257,#258),#17330,
 .F.);
#18137=ADVANCED_FACE('',(#2109),#971,.F.);
#18138=ADVANCED_FACE('',(#2110,#259),#674,.T.);
#18305=CLOSED_SHELL('',(#18111,#18112,#18113,#18114,#18115,#18116,#18117,
#18118,#18119,#18120,#18121,#18122,#18123,#18124,#18125,#18126,#18127,#18128,
#18129,#18130,#18131,#18132,#18133,#18134,#18135,#18136,#18137,#18138));
#19440=AXIS2_PLACEMENT_3D('',#58979,#22656,#22657);
#19441=AXIS2_PLACEMENT_3D('',#58980,#22658,#22659);
#19442=AXIS2_PLACEMENT_3D('',#58983,#22660,#22661);
#19443=AXIS2_PLACEMENT_3D('',#58984,#22662,#22663);
#19444=AXIS2_PLACEMENT_3D('',#58985,#22664,#22665);
#19445=AXIS2_PLACEMENT_3D('',#58989,#22667,#22668);
#19446=AXIS2_PLACEMENT_3D('',#58991,#22670,#22671);
#19447=AXIS2_PLACEMENT_3D('',#58992,#22672,#22673);
#19448=AXIS2_PLACEMENT_3D('',#58993,#22674,#22675);
#19449=AXIS2_PLACEMENT_3D('',#58996,#22676,#22677);
#19450=AXIS2_PLACEMENT_3D('',#58997,#22678,#22679);
#19451=AXIS2_PLACEMENT_3D('',#58998,#22680,#22681);
#19452=AXIS2_PLACEMENT_3D('',#59002,#22683,#22684);
#19453=AXIS2_PLACEMENT_3D('',#59004,#22686,#22687);
#19454=AXIS2_PLACEMENT_3D('',#59005,#22688,#22689);
#19455=AXIS2_PLACEMENT_3D('',#59006,#22690,#22691);
#19456=AXIS2_PLACEMENT_3D('',#59009,#22692,#22693);
#19457=AXIS2_PLACEMENT_3D('',#59010,#22694,#22695);
#19458=AXIS2_PLACEMENT_3D('',#59011,#22696,#22697);
#19459=AXIS2_PLACEMENT_3D('',#59015,#22699,#22700);
#19460=AXIS2_PLACEMENT_3D('',#59017,#22702,#22703);
#19461=AXIS2_PLACEMENT_3D('',#59018,#22704,#22705);
#19462=AXIS2_PLACEMENT_3D('',#59019,#22706,#22707);
#19463=AXIS2_PLACEMENT_3D('',#59022,#22708,#22709);
#19464=AXIS2_PLACEMENT_3D('',#59023,#22710,#22711);
#19465=AXIS2_PLACEMENT_3D('',#59024,#22712,#22713);
#19466=AXIS2_PLACEMENT_3D('',#59028,#22715,#22716);
#19467=AXIS2_PLACEMENT_3D('',#59030,#22718,#22719);
#19468=AXIS2_PLACEMENT_3D('',#59031,#22720,#22721);
#19469=AXIS2_PLACEMENT_3D('',#59032,#22722,#22723);
#19470=AXIS2_PLACEMENT_3D('',#59111,#22725,#22726);
#19471=AXIS2_PLACEMENT_3D('',#59190,#22728,#22729);
#19472=AXIS2_PLACEMENT_3D('',#59272,#22731,#22732);
#19473=AXIS2_PLACEMENT_3D('',#59351,#22734,#22735);
#19474=AXIS2_PLACEMENT_3D('',#59353,#22736,#22737);
#19475=AXIS2_PLACEMENT_3D('',#59357,#22740,#22741);
#19476=AXIS2_PLACEMENT_3D('',#59358,#22742,#22743);
#19477=AXIS2_PLACEMENT_3D('',#59360,#22744,#22745);
#19478=AXIS2_PLACEMENT_3D('',#59361,#22746,#22747);
#19479=AXIS2_PLACEMENT_3D('',#59363,#22748,#22749);
#19480=AXIS2_PLACEMENT_3D('',#59364,#22750,#22751);
#19481=AXIS2_PLACEMENT_3D('',#59366,#22752,#22753);
#19482=AXIS2_PLACEMENT_3D('',#59368,#22755,#22756);
#19483=AXIS2_PLACEMENT_3D('',#59370,#22757,#22758);
#19484=AXIS2_PLACEMENT_3D('',#59373,#22760,#22761);
#19485=AXIS2_PLACEMENT_3D('',#59374,#22762,#22763);
#19486=AXIS2_PLACEMENT_3D('',#59376,#22765,#22766);
#19487=AXIS2_PLACEMENT_3D('',#59378,#22767,#22768);
#19488=AXIS2_PLACEMENT_3D('',#59380,#22770,#22771);
#19489=AXIS2_PLACEMENT_3D('',#59382,#22772,#22773);
#19490=AXIS2_PLACEMENT_3D('',#59383,#22774,#22775);
#19491=AXIS2_PLACEMENT_3D('',#59386,#22777,#22778);
#19492=AXIS2_PLACEMENT_3D('',#59387,#22779,#22780);
#19493=AXIS2_PLACEMENT_3D('',#59391,#22783,#22784);
#19494=AXIS2_PLACEMENT_3D('',#59392,#22785,#22786);
#19495=AXIS2_PLACEMENT_3D('',#59395,#22788,#22789);
#19496=AXIS2_PLACEMENT_3D('',#59396,#22790,#22791);
#22656=DIRECTION('axis',(0.,0.,1.));
#22657=DIRECTION('refdir',(1.,0.,0.));
#22658=DIRECTION('center_axis',(1.,0.,0.));
#22659=DIRECTION('ref_axis',(0.,-1.,1.83697019872103E-16));
#22660=DIRECTION('center_axis',(1.,0.,0.));
#22661=DIRECTION('ref_axis',(0.,1.,0.));
#22662=DIRECTION('center_axis',(1.,0.,0.));
#22663=DIRECTION('ref_axis',(0.,-1.,1.83697019872103E-16));
#22664=DIRECTION('center_axis',(1.,0.,0.));
#22665=DIRECTION('ref_axis',(0.,0.707106781186547,-0.707106781186548));
#22666=DIRECTION('',(-1.,0.,0.));
#22667=DIRECTION('center_axis',(1.,0.,0.));
#22668=DIRECTION('ref_axis',(0.,-1.,1.83697019872103E-16));
#22669=DIRECTION('',(1.,0.,0.));
#22670=DIRECTION('center_axis',(1.,0.,0.));
#22671=DIRECTION('ref_axis',(0.,-1.,1.83697019872103E-16));
#22672=DIRECTION('center_axis',(-1.,0.,0.));
#22673=DIRECTION('ref_axis',(0.,1.,0.));
#22674=DIRECTION('center_axis',(1.,0.,0.));
#22675=DIRECTION('ref_axis',(0.,1.22464679914735E-16,1.));
#22676=DIRECTION('center_axis',(1.,0.,0.));
#22677=DIRECTION('ref_axis',(0.,1.,0.));
#22678=DIRECTION('center_axis',(1.,0.,0.));
#22679=DIRECTION('ref_axis',(0.,1.22464679914735E-16,1.));
#22680=DIRECTION('center_axis',(1.,0.,0.));
#22681=DIRECTION('ref_axis',(0.,-0.707106781186548,-0.707106781186547));
#22682=DIRECTION('',(-1.,0.,0.));
#22683=DIRECTION('center_axis',(1.,0.,0.));
#22684=DIRECTION('ref_axis',(0.,1.22464679914735E-16,1.));
#22685=DIRECTION('',(1.,0.,0.));
#22686=DIRECTION('center_axis',(1.,0.,0.));
#22687=DIRECTION('ref_axis',(0.,1.22464679914735E-16,1.));
#22688=DIRECTION('center_axis',(-1.,0.,0.));
#22689=DIRECTION('ref_axis',(0.,1.,0.));
#22690=DIRECTION('center_axis',(1.,0.,0.));
#22691=DIRECTION('ref_axis',(0.,1.,-6.12323399573677E-17));
#22692=DIRECTION('center_axis',(1.,0.,0.));
#22693=DIRECTION('ref_axis',(0.,1.,0.));
#22694=DIRECTION('center_axis',(1.,0.,0.));
#22695=DIRECTION('ref_axis',(0.,1.,-6.12323399573676E-17));
#22696=DIRECTION('center_axis',(1.,0.,0.));
#22697=DIRECTION('ref_axis',(0.,-0.707106781186547,0.707106781186548));
#22698=DIRECTION('',(-1.,0.,0.));
#22699=DIRECTION('center_axis',(1.,0.,0.));
#22700=DIRECTION('ref_axis',(0.,1.,-6.12323399573676E-17));
#22701=DIRECTION('',(1.,0.,0.));
#22702=DIRECTION('center_axis',(1.,0.,0.));
#22703=DIRECTION('ref_axis',(0.,1.,-6.12323399573677E-17));
#22704=DIRECTION('center_axis',(-1.,0.,0.));
#22705=DIRECTION('ref_axis',(0.,1.,0.));
#22706=DIRECTION('center_axis',(1.,0.,0.));
#22707=DIRECTION('ref_axis',(0.,0.,-1.));
#22708=DIRECTION('center_axis',(1.,0.,0.));
#22709=DIRECTION('ref_axis',(0.,1.,0.));
#22710=DIRECTION('center_axis',(1.,0.,0.));
#22711=DIRECTION('ref_axis',(0.,0.,-1.));
#22712=DIRECTION('center_axis',(1.,0.,0.));
#22713=DIRECTION('ref_axis',(0.,0.707106781186548,0.707106781186547));
#22714=DIRECTION('',(-1.,0.,0.));
#22715=DIRECTION('center_axis',(1.,0.,0.));
#22716=DIRECTION('ref_axis',(0.,0.,-1.));
#22717=DIRECTION('',(1.,0.,0.));
#22718=DIRECTION('center_axis',(1.,0.,0.));
#22719=DIRECTION('ref_axis',(0.,0.,-1.));
#22720=DIRECTION('center_axis',(-1.,0.,0.));
#22721=DIRECTION('ref_axis',(0.,1.,0.));
#22722=DIRECTION('center_axis',(0.,-1.,1.83697019872103E-16));
#22723=DIRECTION('ref_axis',(1.,0.,0.));
#22724=DIRECTION('',(0.,-1.,1.83697019872103E-16));
#22725=DIRECTION('center_axis',(0.,1.22464679914735E-16,1.));
#22726=DIRECTION('ref_axis',(1.,0.,0.));
#22727=DIRECTION('',(0.,1.22464679914735E-16,1.));
#22728=DIRECTION('center_axis',(0.,1.,-6.12323399573677E-17));
#22729=DIRECTION('ref_axis',(1.,0.,0.));
#22730=DIRECTION('',(0.,1.,-6.12323399573677E-17));
#22731=DIRECTION('center_axis',(0.,0.,-1.));
#22732=DIRECTION('ref_axis',(1.,0.,0.));
#22733=DIRECTION('',(0.,0.,-1.));
#22734=DIRECTION('center_axis',(1.,0.,0.));
#22735=DIRECTION('ref_axis',(0.,1.,0.));
#22736=DIRECTION('center_axis',(1.,0.,0.));
#22737=DIRECTION('ref_axis',(0.,0.,-1.));
#22738=DIRECTION('',(1.,0.,0.));
#22739=DIRECTION('',(1.,0.,0.));
#22740=DIRECTION('center_axis',(1.,0.,0.));
#22741=DIRECTION('ref_axis',(0.,0.,-1.));
#22742=DIRECTION('center_axis',(-1.,0.,0.));
#22743=DIRECTION('ref_axis',(0.,0.,1.));
#22744=DIRECTION('center_axis',(-1.,0.,0.));
#22745=DIRECTION('ref_axis',(0.,1.,0.));
#22746=DIRECTION('center_axis',(1.,0.,0.));
#22747=DIRECTION('ref_axis',(0.,0.,-1.));
#22748=DIRECTION('center_axis',(1.,0.,0.));
#22749=DIRECTION('ref_axis',(0.,1.,0.));
#22750=DIRECTION('center_axis',(1.,0.,0.));
#22751=DIRECTION('ref_axis',(0.,1.,0.));
#22752=DIRECTION('center_axis',(1.,0.,0.));
#22753=DIRECTION('ref_axis',(0.,0.,-1.));
#22754=DIRECTION('',(-1.,0.,0.));
#22755=DIRECTION('center_axis',(1.,0.,0.));
#22756=DIRECTION('ref_axis',(0.,1.,0.));
#22757=DIRECTION('center_axis',(1.,0.,0.));
#22758=DIRECTION('ref_axis',(0.,0.,-1.));
#22759=DIRECTION('',(-0.707106781186547,0.707106781186548,8.65956056235494E-17));
#22760=DIRECTION('center_axis',(1.,0.,0.));
#22761=DIRECTION('ref_axis',(0.,0.,-1.));
#22762=DIRECTION('center_axis',(1.,0.,0.));
#22763=DIRECTION('ref_axis',(0.,1.,0.));
#22764=DIRECTION('',(-1.,0.,0.));
#22765=DIRECTION('center_axis',(-1.,0.,0.));
#22766=DIRECTION('ref_axis',(0.,1.,0.));
#22767=DIRECTION('center_axis',(1.,0.,0.));
#22768=DIRECTION('ref_axis',(0.,0.,-1.));
#22769=DIRECTION('',(-0.707106781186548,-0.707106781186548,-8.65956056235493E-17));
#22770=DIRECTION('center_axis',(1.,0.,0.));
#22771=DIRECTION('ref_axis',(0.,0.,-1.));
#22772=DIRECTION('center_axis',(1.,0.,0.));
#22773=DIRECTION('ref_axis',(0.,0.,-1.));
#22774=DIRECTION('center_axis',(1.,0.,0.));
#22775=DIRECTION('ref_axis',(0.,1.,0.));
#22776=DIRECTION('',(-0.707106781186546,0.707106781186549,8.65956056235495E-17));
#22777=DIRECTION('center_axis',(1.,0.,0.));
#22778=DIRECTION('ref_axis',(0.,0.,-1.));
#22779=DIRECTION('center_axis',(1.,0.,0.));
#22780=DIRECTION('ref_axis',(0.,1.,0.));
#22781=DIRECTION('',(-1.,0.,0.));
#22782=DIRECTION('',(-1.,0.,0.));
#22783=DIRECTION('center_axis',(1.,0.,0.));
#22784=DIRECTION('ref_axis',(0.,0.,-1.));
#22785=DIRECTION('center_axis',(-1.,0.,0.));
#22786=DIRECTION('ref_axis',(0.,1.,0.));
#22787=DIRECTION('',(-0.707106781186546,-0.707106781186549,-8.65956056235495E-17));
#22788=DIRECTION('center_axis',(1.,0.,0.));
#22789=DIRECTION('ref_axis',(0.,0.,-1.));
#22790=DIRECTION('center_axis',(-1.,0.,0.));
#22791=DIRECTION('ref_axis',(0.,0.,1.));
#58979=CARTESIAN_POINT('',(0.,0.,0.));
#58980=CARTESIAN_POINT('Origin',(0.8,3.90322943214974,-3.90322943214974));
#58981=CARTESIAN_POINT('',(0.8,3.45653456843748,-4.3038086362194));
#58982=CARTESIAN_POINT('',(0.8,4.3038086362194,-3.45653456843748));
#58983=CARTESIAN_POINT('Origin',(0.8,0.,0.));
#58984=CARTESIAN_POINT('Origin',(0.8,3.90322943214974,-3.90322943214974));
#58985=CARTESIAN_POINT('Origin',(0.8,3.90322943214974,-3.90322943214974));
#58986=CARTESIAN_POINT('',(9.7,3.45653456843748,-4.3038086362194));
#58987=CARTESIAN_POINT('',(0.8,3.45653456843748,-4.3038086362194));
#58988=CARTESIAN_POINT('',(9.7,4.3038086362194,-3.45653456843748));
#58989=CARTESIAN_POINT('Origin',(9.7,3.90322943214974,-3.90322943214974));
#58990=CARTESIAN_POINT('',(0.8,4.3038086362194,-3.45653456843748));
#58991=CARTESIAN_POINT('Origin',(9.7,3.90322943214974,-3.90322943214974));
#58992=CARTESIAN_POINT('Origin',(9.7,0.,0.));
#58993=CARTESIAN_POINT('Origin',(0.8,-3.90322943214974,-3.90322943214974));
#58994=CARTESIAN_POINT('',(0.8,-4.3038086362194,-3.45653456843748));
#58995=CARTESIAN_POINT('',(0.8,-3.45653456843748,-4.3038086362194));
#58996=CARTESIAN_POINT('Origin',(0.8,0.,0.));
#58997=CARTESIAN_POINT('Origin',(0.8,-3.90322943214974,-3.90322943214974));
#58998=CARTESIAN_POINT('Origin',(0.8,-3.90322943214974,-3.90322943214974));
#58999=CARTESIAN_POINT('',(9.7,-4.3038086362194,-3.45653456843748));
#59000=CARTESIAN_POINT('',(0.8,-4.3038086362194,-3.45653456843748));
#59001=CARTESIAN_POINT('',(9.7,-3.45653456843748,-4.3038086362194));
#59002=CARTESIAN_POINT('Origin',(9.7,-3.90322943214974,-3.90322943214974));
#59003=CARTESIAN_POINT('',(0.8,-3.45653456843748,-4.3038086362194));
#59004=CARTESIAN_POINT('Origin',(9.7,-3.90322943214974,-3.90322943214974));
#59005=CARTESIAN_POINT('Origin',(9.7,0.,0.));
#59006=CARTESIAN_POINT('Origin',(0.8,-3.90322943214974,3.90322943214974));
#59007=CARTESIAN_POINT('',(0.8,-3.45653456843748,4.3038086362194));
#59008=CARTESIAN_POINT('',(0.8,-4.3038086362194,3.45653456843748));
#59009=CARTESIAN_POINT('Origin',(0.8,0.,0.));
#59010=CARTESIAN_POINT('Origin',(0.8,-3.90322943214974,3.90322943214974));
#59011=CARTESIAN_POINT('Origin',(0.8,-3.90322943214974,3.90322943214974));
#59012=CARTESIAN_POINT('',(9.7,-3.45653456843748,4.3038086362194));
#59013=CARTESIAN_POINT('',(0.8,-3.45653456843748,4.3038086362194));
#59014=CARTESIAN_POINT('',(9.7,-4.3038086362194,3.45653456843748));
#59015=CARTESIAN_POINT('Origin',(9.7,-3.90322943214974,3.90322943214974));
#59016=CARTESIAN_POINT('',(0.8,-4.3038086362194,3.45653456843748));
#59017=CARTESIAN_POINT('Origin',(9.7,-3.90322943214974,3.90322943214974));
#59018=CARTESIAN_POINT('Origin',(9.7,0.,0.));
#59019=CARTESIAN_POINT('Origin',(0.8,3.90322943214974,3.90322943214974));
#59020=CARTESIAN_POINT('',(0.8,4.3038086362194,3.45653456843748));
#59021=CARTESIAN_POINT('',(0.8,3.45653456843748,4.3038086362194));
#59022=CARTESIAN_POINT('Origin',(0.8,0.,0.));
#59023=CARTESIAN_POINT('Origin',(0.8,3.90322943214974,3.90322943214974));
#59024=CARTESIAN_POINT('Origin',(0.8,3.90322943214974,3.90322943214974));
#59025=CARTESIAN_POINT('',(9.7,4.3038086362194,3.45653456843748));
#59026=CARTESIAN_POINT('',(0.8,4.3038086362194,3.45653456843748));
#59027=CARTESIAN_POINT('',(9.7,3.45653456843748,4.3038086362194));
#59028=CARTESIAN_POINT('Origin',(9.7,3.90322943214974,3.90322943214974));
#59029=CARTESIAN_POINT('',(0.8,3.45653456843748,4.3038086362194));
#59030=CARTESIAN_POINT('Origin',(9.7,3.90322943214974,3.90322943214974));
#59031=CARTESIAN_POINT('Origin',(9.7,0.,0.));
#59032=CARTESIAN_POINT('Origin',(5.25,8.45,-1.55223981791927E-15));
#59033=CARTESIAN_POINT('',(6.35,8.45,-1.55223981791927E-15));
#59034=CARTESIAN_POINT('',(4.15,8.45,-1.41752867001306E-15));
#59035=CARTESIAN_POINT('Ctrl Pts',(6.35,8.45,-1.70002900645727E-15));
#59036=CARTESIAN_POINT('Ctrl Pts',(6.35,8.45,0.138286410729708));
#59037=CARTESIAN_POINT('Ctrl Pts',(6.32233132681,8.44625875235353,0.285683724538777));
#59038=CARTESIAN_POINT('Ctrl Pts',(6.21002324830763,8.4327360375918,0.556655210212817));
#59039=CARTESIAN_POINT('Ctrl Pts',(6.12539248344495,8.42314504656407,0.680242435165457));
#59040=CARTESIAN_POINT('Ctrl Pts',(5.93024147512979,8.40510492225533,0.875393443480616));
#59041=CARTESIAN_POINT('Ctrl Pts',(5.80665466688422,8.39547821560232,0.96002345589192));
#59042=CARTESIAN_POINT('Ctrl Pts',(5.53568459489851,8.381873644329,1.07233098368286));
#59043=CARTESIAN_POINT('Ctrl Pts',(5.38828777132263,8.37809644251008,1.1));
#59044=CARTESIAN_POINT('Ctrl Pts',(5.11171222867737,8.37809644251008,1.1));
#59045=CARTESIAN_POINT('Ctrl Pts',(4.96431540510149,8.381873644329,1.07233098368286));
#59046=CARTESIAN_POINT('Ctrl Pts',(4.69334533311577,8.39547821560232,0.960023455891919));
#59047=CARTESIAN_POINT('Ctrl Pts',(4.56975852487021,8.40510492225533,0.875393443480615));
#59048=CARTESIAN_POINT('Ctrl Pts',(4.37460751655505,8.42314504656407,0.680242435165457));
#59049=CARTESIAN_POINT('Ctrl Pts',(4.28997675169238,8.4327360375918,0.556655210212818));
#59050=CARTESIAN_POINT('Ctrl Pts',(4.17766867319,8.44625875235353,0.285683724538777));
#59051=CARTESIAN_POINT('Ctrl Pts',(4.15,8.45,0.138286410729708));
#59052=CARTESIAN_POINT('Ctrl Pts',(4.15,8.45,-1.42247325030098E-15));
#59053=CARTESIAN_POINT('Ctrl Pts',(4.15,8.45,-1.45716771982052E-15));
#59054=CARTESIAN_POINT('Ctrl Pts',(4.15,8.45,-0.138286410729711));
#59055=CARTESIAN_POINT('Ctrl Pts',(4.17766867319,8.44625875235353,-0.28568372453878));
#59056=CARTESIAN_POINT('Ctrl Pts',(4.28997675169238,8.4327360375918,-0.556655210212821));
#59057=CARTESIAN_POINT('Ctrl Pts',(4.37460751655505,8.42314504656407,-0.68024243516546));
#59058=CARTESIAN_POINT('Ctrl Pts',(4.56975852487021,8.40510492225533,-0.875393443480618));
#59059=CARTESIAN_POINT('Ctrl Pts',(4.69334533311577,8.39547821560232,-0.960023455891922));
#59060=CARTESIAN_POINT('Ctrl Pts',(4.96431540510148,8.381873644329,-1.07233098368286));
#59061=CARTESIAN_POINT('Ctrl Pts',(5.11171222867737,8.37809644251008,-1.1));
#59062=CARTESIAN_POINT('Ctrl Pts',(5.25,8.37809644251008,-1.1));
#59063=CARTESIAN_POINT('Ctrl Pts',(5.38828777132263,8.37809644251008,-1.1));
#59064=CARTESIAN_POINT('Ctrl Pts',(5.53568459489851,8.381873644329,-1.07233098368286));
#59065=CARTESIAN_POINT('Ctrl Pts',(5.80665466688422,8.39547821560232,-0.960023455891923));
#59066=CARTESIAN_POINT('Ctrl Pts',(5.93024147512979,8.40510492225533,-0.875393443480619));
#59067=CARTESIAN_POINT('Ctrl Pts',(6.12539248344495,8.42314504656407,-0.68024243516546));
#59068=CARTESIAN_POINT('Ctrl Pts',(6.21002324830763,8.4327360375918,-0.556655210212821));
#59069=CARTESIAN_POINT('Ctrl Pts',(6.32233132681,8.44625875235353,-0.285683724538781));
#59070=CARTESIAN_POINT('Ctrl Pts',(6.35,8.45,-0.138286410729711));
#59071=CARTESIAN_POINT('Ctrl Pts',(6.35,8.45,-1.59594559789866E-15));
#59072=CARTESIAN_POINT('',(4.15,5.52,-1.14681809587245E-15));
#59073=CARTESIAN_POINT('',(4.15,8.45,-1.68695096582548E-15));
#59074=CARTESIAN_POINT('',(5.25,5.40928830808638,-1.1));
#59075=CARTESIAN_POINT('Ctrl Pts',(5.25,5.40928830808638,-1.1));
#59076=CARTESIAN_POINT('Ctrl Pts',(5.11147809944016,5.40928830808638,-1.1));
#59077=CARTESIAN_POINT('Ctrl Pts',(4.9639846961023,5.41516098360831,-1.07224024467438));
#59078=CARTESIAN_POINT('Ctrl Pts',(4.69308215533071,5.43620465823388,-0.959867948076927));
#59079=CARTESIAN_POINT('Ctrl Pts',(4.569639996971,5.45105349297774,-0.875274915581407));
#59080=CARTESIAN_POINT('Ctrl Pts',(4.37473046520206,5.47879477947926,-0.68036538381247));
#59081=CARTESIAN_POINT('Ctrl Pts',(4.29013321807171,5.4935138828468,-0.556920939780125));
#59082=CARTESIAN_POINT('Ctrl Pts',(4.17775786268853,5.51425912806026,-0.286010457396549));
#59083=CARTESIAN_POINT('Ctrl Pts',(4.15,5.52,-0.138514252542119));
#59084=CARTESIAN_POINT('Ctrl Pts',(4.15,5.52,-1.17961196366423E-15));
#59085=CARTESIAN_POINT('Ctrl Pts',(4.15,5.52,-1.21430643318376E-15));
#59086=CARTESIAN_POINT('Ctrl Pts',(4.15,5.52,0.138514252542116));
#59087=CARTESIAN_POINT('Ctrl Pts',(4.17775786268853,5.51425912806026,0.286010457396547));
#59088=CARTESIAN_POINT('Ctrl Pts',(4.29013321807171,5.4935138828468,0.556920939780123));
#59089=CARTESIAN_POINT('Ctrl Pts',(4.37473046520206,5.47879477947926,0.680365383812468));
#59090=CARTESIAN_POINT('Ctrl Pts',(4.569639996971,5.45105349297774,0.875274915581405));
#59091=CARTESIAN_POINT('Ctrl Pts',(4.69308215533071,5.43620465823388,0.959867948076925));
#59092=CARTESIAN_POINT('Ctrl Pts',(4.9639846961023,5.41516098360831,1.07224024467438));
#59093=CARTESIAN_POINT('Ctrl Pts',(5.11147809944016,5.40928830808638,1.1));
#59094=CARTESIAN_POINT('Ctrl Pts',(5.38852190055984,5.40928830808638,1.1));
#59095=CARTESIAN_POINT('Ctrl Pts',(5.5360153038977,5.41516098360831,1.07224024467438));
#59096=CARTESIAN_POINT('Ctrl Pts',(5.80691784466929,5.43620465823388,0.959867948076925));
#59097=CARTESIAN_POINT('Ctrl Pts',(5.930360003029,5.45105349297774,0.875274915581405));
#59098=CARTESIAN_POINT('Ctrl Pts',(6.12526953479794,5.47879477947926,0.680365383812468));
#59099=CARTESIAN_POINT('Ctrl Pts',(6.20986678192829,5.4935138828468,0.556920939780123));
#59100=CARTESIAN_POINT('Ctrl Pts',(6.32224213731147,5.51425912806026,0.286010457396547));
#59101=CARTESIAN_POINT('Ctrl Pts',(6.35,5.52,0.138514252542117));
#59102=CARTESIAN_POINT('Ctrl Pts',(6.35,5.52,-0.138514252542118));
#59103=CARTESIAN_POINT('Ctrl Pts',(6.32224213731147,5.51425912806026,-0.286010457396548));
#59104=CARTESIAN_POINT('Ctrl Pts',(6.20986678192829,5.4935138828468,-0.556920939780125));
#59105=CARTESIAN_POINT('Ctrl Pts',(6.12526953479794,5.47879477947926,-0.68036538381247));
#59106=CARTESIAN_POINT('Ctrl Pts',(5.930360003029,5.45105349297774,-0.875274915581407));
#59107=CARTESIAN_POINT('Ctrl Pts',(5.80691784466929,5.43620465823388,-0.959867948076927));
#59108=CARTESIAN_POINT('Ctrl Pts',(5.5360153038977,5.41516098360831,-1.07224024467438));
#59109=CARTESIAN_POINT('Ctrl Pts',(5.38852190055984,5.40928830808638,-1.1));
#59110=CARTESIAN_POINT('Ctrl Pts',(5.25,5.40928830808638,-1.1));
#59111=CARTESIAN_POINT('Origin',(5.25,-1.03482654527951E-15,-8.45));
#59112=CARTESIAN_POINT('',(6.35,-1.03482654527951E-15,-8.45));
#59113=CARTESIAN_POINT('',(4.15,-9.00115397373305E-16,-8.45));
#59114=CARTESIAN_POINT('Ctrl Pts',(6.35,-9.71445146547012E-16,-8.45));
#59115=CARTESIAN_POINT('Ctrl Pts',(6.35,0.138286410729709,-8.45));
#59116=CARTESIAN_POINT('Ctrl Pts',(6.32233132681,0.285683724538778,-8.44625875235353));
#59117=CARTESIAN_POINT('Ctrl Pts',(6.21002324830763,0.556655210212818,-8.4327360375918));
#59118=CARTESIAN_POINT('Ctrl Pts',(6.12539248344495,0.680242435165458,-8.42314504656407));
#59119=CARTESIAN_POINT('Ctrl Pts',(5.93024147512979,0.875393443480616,-8.40510492225533));
#59120=CARTESIAN_POINT('Ctrl Pts',(5.80665466688423,0.96002345589192,-8.39547821560232));
#59121=CARTESIAN_POINT('Ctrl Pts',(5.53568459489851,1.07233098368286,-8.381873644329));
#59122=CARTESIAN_POINT('Ctrl Pts',(5.38828777132263,1.1,-8.37809644251008));
#59123=CARTESIAN_POINT('Ctrl Pts',(5.11171222867737,1.1,-8.37809644251008));
#59124=CARTESIAN_POINT('Ctrl Pts',(4.96431540510149,1.07233098368286,-8.381873644329));
#59125=CARTESIAN_POINT('Ctrl Pts',(4.69334533311577,0.960023455891919,-8.39547821560232));
#59126=CARTESIAN_POINT('Ctrl Pts',(4.56975852487021,0.875393443480616,-8.40510492225533));
#59127=CARTESIAN_POINT('Ctrl Pts',(4.37460751655505,0.680242435165458,-8.42314504656407));
#59128=CARTESIAN_POINT('Ctrl Pts',(4.28997675169238,0.556655210212818,-8.4327360375918));
#59129=CARTESIAN_POINT('Ctrl Pts',(4.17766867319,0.285683724538778,-8.44625875235353));
#59130=CARTESIAN_POINT('Ctrl Pts',(4.15,0.138286410729709,-8.45));
#59131=CARTESIAN_POINT('Ctrl Pts',(4.15,-5.55111512312578E-16,-8.45));
#59132=CARTESIAN_POINT('Ctrl Pts',(4.15,-8.32667268468867E-16,-8.45));
#59133=CARTESIAN_POINT('Ctrl Pts',(4.15,-0.13828641072971,-8.45));
#59134=CARTESIAN_POINT('Ctrl Pts',(4.17766867319,-0.28568372453878,-8.44625875235353));
#59135=CARTESIAN_POINT('Ctrl Pts',(4.28997675169238,-0.55665521021282,-8.4327360375918));
#59136=CARTESIAN_POINT('Ctrl Pts',(4.37460751655505,-0.680242435165459,
-8.42314504656407));
#59137=CARTESIAN_POINT('Ctrl Pts',(4.56975852487021,-0.875393443480618,
-8.40510492225533));
#59138=CARTESIAN_POINT('Ctrl Pts',(4.69334533311577,-0.960023455891921,
-8.39547821560232));
#59139=CARTESIAN_POINT('Ctrl Pts',(4.96431540510148,-1.07233098368286,-8.381873644329));
#59140=CARTESIAN_POINT('Ctrl Pts',(5.11171222867737,-1.1,-8.37809644251008));
#59141=CARTESIAN_POINT('Ctrl Pts',(5.25,-1.1,-8.37809644251008));
#59142=CARTESIAN_POINT('Ctrl Pts',(5.38828777132263,-1.1,-8.37809644251008));
#59143=CARTESIAN_POINT('Ctrl Pts',(5.53568459489851,-1.07233098368286,-8.381873644329));
#59144=CARTESIAN_POINT('Ctrl Pts',(5.80665466688422,-0.960023455891922,
-8.39547821560232));
#59145=CARTESIAN_POINT('Ctrl Pts',(5.93024147512979,-0.875393443480618,
-8.40510492225533));
#59146=CARTESIAN_POINT('Ctrl Pts',(6.12539248344495,-0.68024243516546,-8.42314504656407));
#59147=CARTESIAN_POINT('Ctrl Pts',(6.21002324830763,-0.55665521021282,-8.4327360375918));
#59148=CARTESIAN_POINT('Ctrl Pts',(6.32233132681,-0.28568372453878,-8.44625875235353));
#59149=CARTESIAN_POINT('Ctrl Pts',(6.35,-0.138286410729711,-8.45));
#59150=CARTESIAN_POINT('Ctrl Pts',(6.35,-1.14491749414469E-15,-8.45));
#59151=CARTESIAN_POINT('',(4.15,-7.86997255232671E-16,-5.52));
#59152=CARTESIAN_POINT('',(4.15,-1.16953769318572E-15,-8.45));
#59153=CARTESIAN_POINT('',(5.25,-1.1,-5.40928830808638));
#59154=CARTESIAN_POINT('Ctrl Pts',(5.25,-1.1,-5.40928830808638));
#59155=CARTESIAN_POINT('Ctrl Pts',(5.11147809944016,-1.1,-5.40928830808638));
#59156=CARTESIAN_POINT('Ctrl Pts',(4.9639846961023,-1.07224024467438,-5.41516098360831));
#59157=CARTESIAN_POINT('Ctrl Pts',(4.69308215533071,-0.959867948076927,
-5.43620465823388));
#59158=CARTESIAN_POINT('Ctrl Pts',(4.569639996971,-0.875274915581407,-5.45105349297774));
#59159=CARTESIAN_POINT('Ctrl Pts',(4.37473046520206,-0.68036538381247,-5.47879477947926));
#59160=CARTESIAN_POINT('Ctrl Pts',(4.29013321807171,-0.556920939780125,
-5.4935138828468));
#59161=CARTESIAN_POINT('Ctrl Pts',(4.17775786268853,-0.286010457396548,
-5.51425912806026));
#59162=CARTESIAN_POINT('Ctrl Pts',(4.15,-0.138514252542118,-5.52));
#59163=CARTESIAN_POINT('Ctrl Pts',(4.15,-8.67361737988404E-16,-5.52));
#59164=CARTESIAN_POINT('Ctrl Pts',(4.15,-7.63278329429795E-16,-5.52));
#59165=CARTESIAN_POINT('Ctrl Pts',(4.15,0.138514252542117,-5.52));
#59166=CARTESIAN_POINT('Ctrl Pts',(4.17775786268853,0.286010457396547,-5.51425912806026));
#59167=CARTESIAN_POINT('Ctrl Pts',(4.29013321807171,0.556920939780123,-5.4935138828468));
#59168=CARTESIAN_POINT('Ctrl Pts',(4.37473046520206,0.680365383812468,-5.47879477947926));
#59169=CARTESIAN_POINT('Ctrl Pts',(4.569639996971,0.875274915581405,-5.45105349297774));
#59170=CARTESIAN_POINT('Ctrl Pts',(4.69308215533071,0.959867948076925,-5.43620465823388));
#59171=CARTESIAN_POINT('Ctrl Pts',(4.9639846961023,1.07224024467438,-5.41516098360831));
#59172=CARTESIAN_POINT('Ctrl Pts',(5.11147809944016,1.1,-5.40928830808638));
#59173=CARTESIAN_POINT('Ctrl Pts',(5.38852190055984,1.1,-5.40928830808638));
#59174=CARTESIAN_POINT('Ctrl Pts',(5.5360153038977,1.07224024467438,-5.41516098360831));
#59175=CARTESIAN_POINT('Ctrl Pts',(5.80691784466929,0.959867948076925,-5.43620465823388));
#59176=CARTESIAN_POINT('Ctrl Pts',(5.930360003029,0.875274915581406,-5.45105349297774));
#59177=CARTESIAN_POINT('Ctrl Pts',(6.12526953479794,0.680365383812468,-5.47879477947926));
#59178=CARTESIAN_POINT('Ctrl Pts',(6.20986678192829,0.556920939780123,-5.4935138828468));
#59179=CARTESIAN_POINT('Ctrl Pts',(6.32224213731147,0.286010457396547,-5.51425912806026));
#59180=CARTESIAN_POINT('Ctrl Pts',(6.35,0.138514252542117,-5.52));
#59181=CARTESIAN_POINT('Ctrl Pts',(6.35,-0.138514252542118,-5.52));
#59182=CARTESIAN_POINT('Ctrl Pts',(6.32224213731147,-0.286010457396548,
-5.51425912806026));
#59183=CARTESIAN_POINT('Ctrl Pts',(6.20986678192829,-0.556920939780125,
-5.4935138828468));
#59184=CARTESIAN_POINT('Ctrl Pts',(6.12526953479794,-0.68036538381247,-5.47879477947926));
#59185=CARTESIAN_POINT('Ctrl Pts',(5.930360003029,-0.875274915581407,-5.45105349297774));
#59186=CARTESIAN_POINT('Ctrl Pts',(5.80691784466929,-0.959867948076927,
-5.43620465823388));
#59187=CARTESIAN_POINT('Ctrl Pts',(5.5360153038977,-1.07224024467438,-5.41516098360831));
#59188=CARTESIAN_POINT('Ctrl Pts',(5.38852190055984,-1.1,-5.40928830808638));
#59189=CARTESIAN_POINT('Ctrl Pts',(5.25,-1.1,-5.40928830808638));
#59190=CARTESIAN_POINT('Origin',(5.25,-8.45,5.17413272639757E-16));
#59191=CARTESIAN_POINT('',(6.35,-8.45,5.17413272639757E-16));
#59192=CARTESIAN_POINT('',(4.15,-8.45,3.82702124733548E-16));
#59193=CARTESIAN_POINT('Ctrl Pts',(6.35,-8.45,6.59194920871187E-16));
#59194=CARTESIAN_POINT('Ctrl Pts',(6.35,-8.45,-0.138286410729709));
#59195=CARTESIAN_POINT('Ctrl Pts',(6.32233132681,-8.44625875235353,-0.285683724538778));
#59196=CARTESIAN_POINT('Ctrl Pts',(6.21002324830763,-8.4327360375918,-0.556655210212818));
#59197=CARTESIAN_POINT('Ctrl Pts',(6.12539248344495,-8.42314504656407,-0.680242435165458));
#59198=CARTESIAN_POINT('Ctrl Pts',(5.93024147512979,-8.40510492225533,-0.875393443480617));
#59199=CARTESIAN_POINT('Ctrl Pts',(5.80665466688422,-8.39547821560232,-0.960023455891921));
#59200=CARTESIAN_POINT('Ctrl Pts',(5.53568459489851,-8.381873644329,-1.07233098368286));
#59201=CARTESIAN_POINT('Ctrl Pts',(5.38828777132263,-8.37809644251008,-1.1));
#59202=CARTESIAN_POINT('Ctrl Pts',(5.11171222867737,-8.37809644251008,-1.1));
#59203=CARTESIAN_POINT('Ctrl Pts',(4.96431540510149,-8.381873644329,-1.07233098368286));
#59204=CARTESIAN_POINT('Ctrl Pts',(4.69334533311577,-8.39547821560232,-0.96002345589192));
#59205=CARTESIAN_POINT('Ctrl Pts',(4.56975852487021,-8.40510492225533,-0.875393443480617));
#59206=CARTESIAN_POINT('Ctrl Pts',(4.37460751655505,-8.42314504656407,-0.680242435165458));
#59207=CARTESIAN_POINT('Ctrl Pts',(4.28997675169238,-8.4327360375918,-0.556655210212819));
#59208=CARTESIAN_POINT('Ctrl Pts',(4.17766867319,-8.44625875235353,-0.285683724538779));
#59209=CARTESIAN_POINT('Ctrl Pts',(4.15,-8.45,-0.138286410729709));
#59210=CARTESIAN_POINT('Ctrl Pts',(4.15,-8.45,3.46944695195361E-16));
#59211=CARTESIAN_POINT('Ctrl Pts',(4.15,-8.45,4.85722573273506E-16));
#59212=CARTESIAN_POINT('Ctrl Pts',(4.15,-8.45,0.13828641072971));
#59213=CARTESIAN_POINT('Ctrl Pts',(4.17766867319,-8.44625875235353,0.285683724538779));
#59214=CARTESIAN_POINT('Ctrl Pts',(4.28997675169238,-8.4327360375918,0.55665521021282));
#59215=CARTESIAN_POINT('Ctrl Pts',(4.37460751655505,-8.42314504656407,0.680242435165459));
#59216=CARTESIAN_POINT('Ctrl Pts',(4.56975852487021,-8.40510492225533,0.875393443480617));
#59217=CARTESIAN_POINT('Ctrl Pts',(4.69334533311577,-8.39547821560232,0.960023455891921));
#59218=CARTESIAN_POINT('Ctrl Pts',(4.96431540510149,-8.381873644329,1.07233098368286));
#59219=CARTESIAN_POINT('Ctrl Pts',(5.11171222867737,-8.37809644251008,1.1));
#59220=CARTESIAN_POINT('Ctrl Pts',(5.25,-8.37809644251008,1.1));
#59221=CARTESIAN_POINT('Ctrl Pts',(5.38828777132263,-8.37809644251008,1.1));
#59222=CARTESIAN_POINT('Ctrl Pts',(5.53568459489851,-8.381873644329,1.07233098368286));
#59223=CARTESIAN_POINT('Ctrl Pts',(5.80665466688422,-8.39547821560232,0.960023455891922));
#59224=CARTESIAN_POINT('Ctrl Pts',(5.93024147512979,-8.40510492225533,0.875393443480618));
#59225=CARTESIAN_POINT('Ctrl Pts',(6.12539248344495,-8.42314504656407,0.680242435165459));
#59226=CARTESIAN_POINT('Ctrl Pts',(6.21002324830763,-8.4327360375918,0.55665521021282));
#59227=CARTESIAN_POINT('Ctrl Pts',(6.32233132681,-8.44625875235353,0.28568372453878));
#59228=CARTESIAN_POINT('Ctrl Pts',(6.35,-8.45,0.13828641072971));
#59229=CARTESIAN_POINT('Ctrl Pts',(6.35,-8.45,5.20417042793042E-16));
#59230=CARTESIAN_POINT('',(4.15,-5.52,4.9656535363196E-16));
#59231=CARTESIAN_POINT('',(4.15,-8.45,6.52124420545966E-16));
#59232=CARTESIAN_POINT('',(5.25,-5.40928830808638,1.1));
#59233=CARTESIAN_POINT('Ctrl Pts',(5.25,-5.40928830808638,1.1));
#59234=CARTESIAN_POINT('Ctrl Pts',(5.11147809944016,-5.40928830808638,1.1));
#59235=CARTESIAN_POINT('Ctrl Pts',(4.9639846961023,-5.41516098360831,1.07224024467438));
#59236=CARTESIAN_POINT('Ctrl Pts',(4.69308215533071,-5.43620465823388,0.959867948076926));
#59237=CARTESIAN_POINT('Ctrl Pts',(4.569639996971,-5.45105349297774,0.875274915581407));
#59238=CARTESIAN_POINT('Ctrl Pts',(4.37473046520206,-5.47879477947926,0.680365383812469));
#59239=CARTESIAN_POINT('Ctrl Pts',(4.29013321807171,-5.4935138828468,0.556920939780125));
#59240=CARTESIAN_POINT('Ctrl Pts',(4.17775786268853,-5.51425912806026,0.286010457396548));
#59241=CARTESIAN_POINT('Ctrl Pts',(4.15,-5.52,0.138514252542118));
#59242=CARTESIAN_POINT('Ctrl Pts',(4.15,-5.52,4.85722573273506E-16));
#59243=CARTESIAN_POINT('',(6.35,-5.52,-3.03308047045133E-16));
#59244=CARTESIAN_POINT('Ctrl Pts',(6.35,-5.52,1.04083408558608E-16));
#59245=CARTESIAN_POINT('Ctrl Pts',(6.35,-5.52,0.138514252542118));
#59246=CARTESIAN_POINT('Ctrl Pts',(6.32224213731147,-5.51425912806026,0.286010457396547));
#59247=CARTESIAN_POINT('Ctrl Pts',(6.20986678192829,-5.4935138828468,0.556920939780124));
#59248=CARTESIAN_POINT('Ctrl Pts',(6.12526953479794,-5.47879477947926,0.680365383812469));
#59249=CARTESIAN_POINT('Ctrl Pts',(5.930360003029,-5.45105349297774,0.875274915581406));
#59250=CARTESIAN_POINT('Ctrl Pts',(5.80691784466929,-5.43620465823388,0.959867948076926));
#59251=CARTESIAN_POINT('Ctrl Pts',(5.5360153038977,-5.41516098360831,1.07224024467438));
#59252=CARTESIAN_POINT('Ctrl Pts',(5.38852190055984,-5.40928830808638,1.1));
#59253=CARTESIAN_POINT('Ctrl Pts',(5.25,-5.40928830808638,1.1));
#59254=CARTESIAN_POINT('Ctrl Pts',(4.15,-5.52,4.85722573273506E-16));
#59255=CARTESIAN_POINT('Ctrl Pts',(4.15,-5.52,-0.138514252542117));
#59256=CARTESIAN_POINT('Ctrl Pts',(4.17775786268853,-5.51425912806026,-0.286010457396547));
#59257=CARTESIAN_POINT('Ctrl Pts',(4.29013321807171,-5.4935138828468,-0.556920939780124));
#59258=CARTESIAN_POINT('Ctrl Pts',(4.37473046520206,-5.47879477947926,-0.680365383812469));
#59259=CARTESIAN_POINT('Ctrl Pts',(4.569639996971,-5.45105349297774,-0.875274915581406));
#59260=CARTESIAN_POINT('Ctrl Pts',(4.69308215533072,-5.43620465823388,-0.959867948076926));
#59261=CARTESIAN_POINT('Ctrl Pts',(4.9639846961023,-5.41516098360831,-1.07224024467438));
#59262=CARTESIAN_POINT('Ctrl Pts',(5.11147809944016,-5.40928830808638,-1.1));
#59263=CARTESIAN_POINT('Ctrl Pts',(5.38852190055984,-5.40928830808638,-1.1));
#59264=CARTESIAN_POINT('Ctrl Pts',(5.5360153038977,-5.41516098360831,-1.07224024467438));
#59265=CARTESIAN_POINT('Ctrl Pts',(5.80691784466929,-5.43620465823388,-0.959867948076926));
#59266=CARTESIAN_POINT('Ctrl Pts',(5.930360003029,-5.45105349297774,-0.875274915581406));
#59267=CARTESIAN_POINT('Ctrl Pts',(6.12526953479794,-5.47879477947926,-0.680365383812469));
#59268=CARTESIAN_POINT('Ctrl Pts',(6.20986678192829,-5.4935138828468,-0.556920939780124));
#59269=CARTESIAN_POINT('Ctrl Pts',(6.32224213731147,-5.51425912806026,-0.286010457396547));
#59270=CARTESIAN_POINT('Ctrl Pts',(6.35,-5.52,-0.138514252542118));
#59271=CARTESIAN_POINT('Ctrl Pts',(6.35,-5.52,1.38777878078145E-16));
#59272=CARTESIAN_POINT('Origin',(5.25,0.,8.45));
#59273=CARTESIAN_POINT('',(6.35,0.,8.45));
#59274=CARTESIAN_POINT('',(4.15,-1.34711147906209E-16,8.45));
#59275=CARTESIAN_POINT('Ctrl Pts',(6.35,-6.93889390390723E-17,8.45));
#59276=CARTESIAN_POINT('Ctrl Pts',(6.35,-0.13828641072971,8.45));
#59277=CARTESIAN_POINT('Ctrl Pts',(6.32233132681,-0.285683724538779,8.44625875235353));
#59278=CARTESIAN_POINT('Ctrl Pts',(6.21002324830763,-0.556655210212819,
8.4327360375918));
#59279=CARTESIAN_POINT('Ctrl Pts',(6.12539248344495,-0.680242435165459,
8.42314504656407));
#59280=CARTESIAN_POINT('Ctrl Pts',(5.93024147512979,-0.875393443480617,
8.40510492225533));
#59281=CARTESIAN_POINT('Ctrl Pts',(5.80665466688422,-0.960023455891921,
8.39547821560232));
#59282=CARTESIAN_POINT('Ctrl Pts',(5.53568459489851,-1.07233098368286,8.381873644329));
#59283=CARTESIAN_POINT('Ctrl Pts',(5.38828777132263,-1.1,8.37809644251008));
#59284=CARTESIAN_POINT('Ctrl Pts',(5.11171222867737,-1.1,8.37809644251008));
#59285=CARTESIAN_POINT('Ctrl Pts',(4.96431540510149,-1.07233098368286,8.381873644329));
#59286=CARTESIAN_POINT('Ctrl Pts',(4.69334533311577,-0.960023455891921,
8.39547821560232));
#59287=CARTESIAN_POINT('Ctrl Pts',(4.56975852487021,-0.875393443480617,
8.40510492225533));
#59288=CARTESIAN_POINT('Ctrl Pts',(4.37460751655505,-0.680242435165459,
8.42314504656407));
#59289=CARTESIAN_POINT('Ctrl Pts',(4.28997675169238,-0.556655210212819,
8.4327360375918));
#59290=CARTESIAN_POINT('Ctrl Pts',(4.17766867319,-0.285683724538779,8.44625875235353));
#59291=CARTESIAN_POINT('Ctrl Pts',(4.15,-0.13828641072971,8.45));
#59292=CARTESIAN_POINT('Ctrl Pts',(4.15,-6.93889390390723E-17,8.45));
#59293=CARTESIAN_POINT('Ctrl Pts',(4.15,-2.08166817117217E-16,8.45));
#59294=CARTESIAN_POINT('Ctrl Pts',(4.15,0.138286410729709,8.45));
#59295=CARTESIAN_POINT('Ctrl Pts',(4.17766867319,0.285683724538779,8.44625875235353));
#59296=CARTESIAN_POINT('Ctrl Pts',(4.28997675169238,0.556655210212819,8.4327360375918));
#59297=CARTESIAN_POINT('Ctrl Pts',(4.37460751655505,0.680242435165458,8.42314504656407));
#59298=CARTESIAN_POINT('Ctrl Pts',(4.56975852487021,0.875393443480617,8.40510492225533));
#59299=CARTESIAN_POINT('Ctrl Pts',(4.69334533311577,0.960023455891921,8.39547821560232));
#59300=CARTESIAN_POINT('Ctrl Pts',(4.96431540510149,1.07233098368286,8.381873644329));
#59301=CARTESIAN_POINT('Ctrl Pts',(5.11171222867737,1.1,8.37809644251008));
#59302=CARTESIAN_POINT('Ctrl Pts',(5.25,1.1,8.37809644251008));
#59303=CARTESIAN_POINT('Ctrl Pts',(5.38828777132263,1.1,8.37809644251008));
#59304=CARTESIAN_POINT('Ctrl Pts',(5.53568459489851,1.07233098368286,8.381873644329));
#59305=CARTESIAN_POINT('Ctrl Pts',(5.80665466688422,0.960023455891921,8.39547821560232));
#59306=CARTESIAN_POINT('Ctrl Pts',(5.93024147512979,0.875393443480617,8.40510492225533));
#59307=CARTESIAN_POINT('Ctrl Pts',(6.12539248344495,0.680242435165459,8.42314504656407));
#59308=CARTESIAN_POINT('Ctrl Pts',(6.21002324830763,0.556655210212819,8.4327360375918));
#59309=CARTESIAN_POINT('Ctrl Pts',(6.32233132681,0.285683724538779,8.44625875235353));
#59310=CARTESIAN_POINT('Ctrl Pts',(6.35,0.138286410729709,8.45));
#59311=CARTESIAN_POINT('Ctrl Pts',(6.35,0.,8.45));
#59312=CARTESIAN_POINT('',(4.15,1.54091747751945E-16,5.52));
#59313=CARTESIAN_POINT('',(4.15,1.34711147906209E-16,8.45));
#59314=CARTESIAN_POINT('',(5.25,1.1,5.40928830808638));
#59315=CARTESIAN_POINT('Ctrl Pts',(5.25,1.1,5.40928830808638));
#59316=CARTESIAN_POINT('Ctrl Pts',(5.11147809944016,1.1,5.40928830808638));
#59317=CARTESIAN_POINT('Ctrl Pts',(4.9639846961023,1.07224024467438,5.41516098360831));
#59318=CARTESIAN_POINT('Ctrl Pts',(4.69308215533071,0.959867948076926,5.43620465823388));
#59319=CARTESIAN_POINT('Ctrl Pts',(4.569639996971,0.875274915581406,5.45105349297774));
#59320=CARTESIAN_POINT('Ctrl Pts',(4.37473046520206,0.680365383812469,5.47879477947926));
#59321=CARTESIAN_POINT('Ctrl Pts',(4.29013321807171,0.556920939780124,5.4935138828468));
#59322=CARTESIAN_POINT('Ctrl Pts',(4.17775786268853,0.286010457396548,5.51425912806026));
#59323=CARTESIAN_POINT('Ctrl Pts',(4.15,0.138514252542118,5.52));
#59324=CARTESIAN_POINT('Ctrl Pts',(4.15,1.73472347597681E-16,5.52));
#59325=CARTESIAN_POINT('Ctrl Pts',(4.15,1.73472347597681E-16,5.52));
#59326=CARTESIAN_POINT('Ctrl Pts',(4.15,-0.138514252542118,5.52));
#59327=CARTESIAN_POINT('Ctrl Pts',(4.17775786268853,-0.286010457396548,
5.51425912806026));
#59328=CARTESIAN_POINT('Ctrl Pts',(4.29013321807171,-0.556920939780124,
5.4935138828468));
#59329=CARTESIAN_POINT('Ctrl Pts',(4.37473046520206,-0.680365383812469,
5.47879477947926));
#59330=CARTESIAN_POINT('Ctrl Pts',(4.569639996971,-0.875274915581406,5.45105349297774));
#59331=CARTESIAN_POINT('Ctrl Pts',(4.69308215533072,-0.959867948076927,
5.43620465823388));
#59332=CARTESIAN_POINT('Ctrl Pts',(4.9639846961023,-1.07224024467438,5.41516098360831));
#59333=CARTESIAN_POINT('Ctrl Pts',(5.11147809944016,-1.1,5.40928830808638));
#59334=CARTESIAN_POINT('Ctrl Pts',(5.38852190055984,-1.1,5.40928830808638));
#59335=CARTESIAN_POINT('Ctrl Pts',(5.53601530389771,-1.07224024467438,5.41516098360831));
#59336=CARTESIAN_POINT('Ctrl Pts',(5.80691784466929,-0.959867948076926,
5.43620465823388));
#59337=CARTESIAN_POINT('Ctrl Pts',(5.930360003029,-0.875274915581406,5.45105349297774));
#59338=CARTESIAN_POINT('Ctrl Pts',(6.12526953479794,-0.680365383812469,
5.47879477947926));
#59339=CARTESIAN_POINT('Ctrl Pts',(6.20986678192829,-0.556920939780124,
5.4935138828468));
#59340=CARTESIAN_POINT('Ctrl Pts',(6.32224213731147,-0.286010457396547,
5.51425912806026));
#59341=CARTESIAN_POINT('Ctrl Pts',(6.35,-0.138514252542118,5.52));
#59342=CARTESIAN_POINT('Ctrl Pts',(6.35,0.138514252542118,5.52));
#59343=CARTESIAN_POINT('Ctrl Pts',(6.32224213731147,0.286010457396547,5.51425912806026));
#59344=CARTESIAN_POINT('Ctrl Pts',(6.20986678192829,0.556920939780124,5.4935138828468));
#59345=CARTESIAN_POINT('Ctrl Pts',(6.12526953479794,0.680365383812469,5.47879477947926));
#59346=CARTESIAN_POINT('Ctrl Pts',(5.930360003029,0.875274915581406,5.45105349297774));
#59347=CARTESIAN_POINT('Ctrl Pts',(5.80691784466929,0.959867948076926,5.43620465823388));
#59348=CARTESIAN_POINT('Ctrl Pts',(5.5360153038977,1.07224024467438,5.41516098360831));
#59349=CARTESIAN_POINT('Ctrl Pts',(5.38852190055984,1.1,5.40928830808638));
#59350=CARTESIAN_POINT('Ctrl Pts',(5.25,1.1,5.40928830808638));
#59351=CARTESIAN_POINT('Origin',(5.25,0.,0.));
#59352=CARTESIAN_POINT('',(3.75,-8.45,-1.03482654527951E-15));
#59353=CARTESIAN_POINT('Origin',(3.75,0.,0.));
#59354=CARTESIAN_POINT('',(5.25,-8.45,-1.03482654527951E-15));
#59355=CARTESIAN_POINT('',(6.75,-8.45,-1.03482654527951E-15));
#59356=CARTESIAN_POINT('',(5.25,-8.45,-1.03482654527951E-15));
#59357=CARTESIAN_POINT('Origin',(6.75,0.,0.));
#59358=CARTESIAN_POINT('Origin',(3.75,9.,0.));
#59359=CARTESIAN_POINT('',(3.75,-8.8,1.07768918324967E-15));
#59360=CARTESIAN_POINT('Origin',(3.75,0.,0.));
#59361=CARTESIAN_POINT('Origin',(6.75,8.45,0.));
#59362=CARTESIAN_POINT('',(6.75,-8.8,-1.07768918324967E-15));
#59363=CARTESIAN_POINT('Origin',(6.75,0.,0.));
#59364=CARTESIAN_POINT('Origin',(5.25,0.,0.));
#59365=CARTESIAN_POINT('',(10.1,-8.8,-1.07768918324967E-15));
#59366=CARTESIAN_POINT('Origin',(10.1,0.,0.));
#59367=CARTESIAN_POINT('',(5.25,-8.8,-1.07768918324967E-15));
#59368=CARTESIAN_POINT('Origin',(0.2,0.,0.));
#59369=CARTESIAN_POINT('',(0.4,-8.8,-1.07768918324967E-15));
#59370=CARTESIAN_POINT('Origin',(0.4,0.,0.));
#59371=CARTESIAN_POINT('',(-1.04083408558608E-16,-8.4,-1.02870331128378E-15));
#59372=CARTESIAN_POINT('',(0.2,-8.6,-1.05319624726672E-15));
#59373=CARTESIAN_POINT('Origin',(0.,0.,0.));
#59374=CARTESIAN_POINT('Origin',(5.25,0.,0.));
#59375=CARTESIAN_POINT('',(5.25,-8.8,-1.07768918324967E-15));
#59376=CARTESIAN_POINT('Origin',(10.3,0.,0.));
#59377=CARTESIAN_POINT('',(10.5,-8.4,-1.02870331128378E-15));
#59378=CARTESIAN_POINT('Origin',(10.5,0.,0.));
#59379=CARTESIAN_POINT('',(10.3,-8.6,-1.05319624726672E-15));
#59380=CARTESIAN_POINT('Origin',(10.5,5.82,0.));
#59381=CARTESIAN_POINT('',(10.5,-5.82,-7.1274443710376E-16));
#59382=CARTESIAN_POINT('Origin',(10.5,0.,0.));
#59383=CARTESIAN_POINT('Origin',(10.35,0.,0.));
#59384=CARTESIAN_POINT('',(10.2,-5.52,-6.76005033129339E-16));
#59385=CARTESIAN_POINT('',(10.35,-5.67,-6.94374735116549E-16));
#59386=CARTESIAN_POINT('Origin',(10.2,0.,0.));
#59387=CARTESIAN_POINT('Origin',(5.25,0.,0.));
#59388=CARTESIAN_POINT('',(5.25,-5.52,-6.76005033129339E-16));
#59389=CARTESIAN_POINT('',(0.3,-5.52,-6.76005033129339E-16));
#59390=CARTESIAN_POINT('',(5.25,-5.52,-6.76005033129339E-16));
#59391=CARTESIAN_POINT('Origin',(0.3,0.,0.));
#59392=CARTESIAN_POINT('Origin',(0.15,0.,0.));
#59393=CARTESIAN_POINT('',(-3.98986399474666E-16,-5.82,-7.1274443710376E-16));
#59394=CARTESIAN_POINT('',(0.15,-5.67,-6.94374735116549E-16));
#59395=CARTESIAN_POINT('Origin',(0.,0.,0.));
#59396=CARTESIAN_POINT('Origin',(0.,8.4,0.));
#60351=UNCERTAINTY_MEASURE_WITH_UNIT(LENGTH_MEASURE(0.01),#60366,
'DISTANCE_ACCURACY_VALUE',
'Maximum model space distance between geometric entities at asserted c
onnectivities');
#60353=UNCERTAINTY_MEASURE_WITH_UNIT(LENGTH_MEASURE(0.01),#60366,
'DISTANCE_ACCURACY_VALUE',
'Maximum model space distance between geometric entities at asserted c
onnectivities');
#60363=(
GEOMETRIC_REPRESENTATION_CONTEXT(3)
GLOBAL_UNCERTAINTY_ASSIGNED_CONTEXT((#60351))
GLOBAL_UNIT_ASSIGNED_CONTEXT((#60366,#60368,#60369))
REPRESENTATION_CONTEXT('','3D')
);
#60365=(
GEOMETRIC_REPRESENTATION_CONTEXT(3)
GLOBAL_UNCERTAINTY_ASSIGNED_CONTEXT((#60353))
GLOBAL_UNIT_ASSIGNED_CONTEXT((#60366,#60368,#60369))
REPRESENTATION_CONTEXT('','3D')
);
#60366=(
LENGTH_UNIT()
NAMED_UNIT(*)
SI_UNIT(.MILLI.,.METRE.)
);
#60368=(
NAMED_UNIT(*)
PLANE_ANGLE_UNIT()
SI_UNIT($,.RADIAN.)
);
#60369=(
NAMED_UNIT(*)
SI_UNIT($,.STERADIAN.)
SOLID_ANGLE_UNIT()
);
#60379=SHAPE_DEFINITION_REPRESENTATION(#60390,#60415);
#60390=PRODUCT_DEFINITION_SHAPE('',$,#60427);
#60415=SHAPE_REPRESENTATION('',(#19440),#60363);
#60417=PRODUCT_DEFINITION_CONTEXT('part definition',#60452,'design');
#60427=PRODUCT_DEFINITION('2026-10-25-00-06-28-201',
'03_Journal_Bearing_D11',#60438,#60417);
#60438=PRODUCT_DEFINITION_FORMATION('',$,#60463);
#60452=APPLICATION_CONTEXT(
'Core Data for Automotive Mechanical Design Process');
#60453=PRODUCT_CONTEXT('part definition',#60452,'mechanical');
#60463=PRODUCT('2026-10-25-00-06-28-201','03_Journal_Bearing_D11',$,(#60453));
#60521=COLOUR_RGB('Grey',0.48,0.52,0.57);
#60522=FILL_AREA_STYLE_COLOUR('',#60521);
#60523=FILL_AREA_STYLE('',(#60522));
#60524=SURFACE_STYLE_FILL_AREA(#60523);
#60525=SURFACE_SIDE_STYLE('',(#60524));
#60526=SURFACE_STYLE_USAGE(.BOTH.,#60525);
#60527=PRESENTATION_STYLE_ASSIGNMENT((#60526));
ENDSEC;
END-ISO-10303-21;
